ISO-10303-21;
HEADER;
/* Generated by software containing ST-Developer
 * from STEP Tools, Inc. (www.steptools.com) 
 */
/* OPTION: using custom renumber hook */

FILE_DESCRIPTION(
/* description */ ('STEP AP242 Edition 2', 'CAx-IF Rec.Pracs.---Representation and Presentation of Product Manufa
cturing Information (PMI)---4.0---2014-10-13', 'CAx-IF Rec.Pracs.---3D Tessellated Geometry---0.4---2014-09-14', '2;1', 'CAx-IF Rec.Pracs.---User Defined Attributes---1.5---2016-08-15'),
/* implementation_level */ '2;1');

FILE_NAME(
/* name */ 'Part 1__PD10218.step',
/* time_stamp */ '2026-10-09T13:59:33Z',
/* author */ (''),
/* organization */ (''),
/* preprocessor_version */ 'ST-DEVELOPER v20',
/* originating_system */ 'ONSHAPE BY PTC INC, 1.221',
/* authorisation */ '  ');

FILE_SCHEMA (('AP242_MANAGED_MODEL_BASED_3D_ENGINEERING_MIM_LF { 1 0 10303 442 3 1 4 }'));
ENDSEC;

DATA;
#184=LINE('',#9422,#468);
#185=LINE('',#9424,#469);
#186=LINE('',#9428,#470);
#187=LINE('',#9432,#471);
#188=LINE('',#9434,#472);
#189=LINE('',#9436,#473);
#190=LINE('',#9440,#474);
#191=LINE('',#9442,#475);
#192=LINE('',#9446,#476);
#193=LINE('',#9448,#477);
#194=LINE('',#9452,#478);
#195=LINE('',#9456,#479);
#196=LINE('',#9458,#480);
#197=LINE('',#9460,#481);
#198=LINE('',#9464,#482);
#199=LINE('',#9468,#483);
#200=LINE('',#9470,#484);
#201=LINE('',#9472,#485);
#202=LINE('',#9476,#486);
#203=LINE('',#9478,#487);
#204=LINE('',#9482,#488);
#205=LINE('',#9486,#489);
#206=LINE('',#9488,#490);
#207=LINE('',#9490,#491);
#208=LINE('',#9494,#492);
#209=LINE('',#9498,#493);
#210=LINE('',#9500,#494);
#211=LINE('',#9504,#495);
#212=LINE('',#9506,#496);
#213=LINE('',#9510,#497);
#214=LINE('',#9512,#498);
#215=LINE('',#9514,#499);
#216=LINE('',#9518,#500);
#217=LINE('',#9520,#501);
#218=LINE('',#9524,#502);
#219=LINE('',#9528,#503);
#220=LINE('',#9530,#504);
#221=LINE('',#9534,#505);
#222=LINE('',#9536,#506);
#223=LINE('',#9540,#507);
#224=LINE('',#9542,#508);
#225=LINE('',#9544,#509);
#226=LINE('',#9662,#510);
#227=LINE('',#9663,#511);
#228=LINE('',#9665,#512);
#229=LINE('',#9667,#513);
#230=LINE('',#9670,#514);
#231=LINE('',#9672,#515);
#232=LINE('',#9675,#516);
#233=LINE('',#9677,#517);
#234=LINE('',#9680,#518);
#235=LINE('',#9682,#519);
#236=LINE('',#9685,#520);
#237=LINE('',#9687,#521);
#238=LINE('',#9690,#522);
#239=LINE('',#9692,#523);
#240=LINE('',#9695,#524);
#241=LINE('',#9697,#525);
#242=LINE('',#9700,#526);
#243=LINE('',#9702,#527);
#244=LINE('',#9705,#528);
#245=LINE('',#9707,#529);
#246=LINE('',#9710,#530);
#247=LINE('',#9712,#531);
#248=LINE('',#9715,#532);
#249=LINE('',#9717,#533);
#250=LINE('',#9720,#534);
#251=LINE('',#9722,#535);
#252=LINE('',#9725,#536);
#253=LINE('',#9727,#537);
#254=LINE('',#9730,#538);
#255=LINE('',#9732,#539);
#256=LINE('',#9735,#540);
#257=LINE('',#9737,#541);
#258=LINE('',#9740,#542);
#259=LINE('',#9742,#543);
#260=LINE('',#9745,#544);
#261=LINE('',#9747,#545);
#262=LINE('',#9750,#546);
#263=LINE('',#9752,#547);
#264=LINE('',#9755,#548);
#265=LINE('',#9757,#549);
#266=LINE('',#9760,#550);
#267=LINE('',#9762,#551);
#268=LINE('',#9765,#552);
#269=LINE('',#9767,#553);
#270=LINE('',#9770,#554);
#271=LINE('',#9772,#555);
#468=VECTOR('',#7586,1.);
#469=VECTOR('',#7587,1.);
#470=VECTOR('',#7592,1.);
#471=VECTOR('',#7595,1.);
#472=VECTOR('',#7598,1.);
#473=VECTOR('',#7599,1.);
#474=VECTOR('',#7604,1.);
#475=VECTOR('',#7605,1.);
#476=VECTOR('',#7610,1.);
#477=VECTOR('',#7611,1.);
#478=VECTOR('',#7616,1.);
#479=VECTOR('',#7619,1.);
#480=VECTOR('',#7622,1.);
#481=VECTOR('',#7623,1.);
#482=VECTOR('',#7628,1.);
#483=VECTOR('',#7631,1.);
#484=VECTOR('',#7634,1.);
#485=VECTOR('',#7635,1.);
#486=VECTOR('',#7640,1.);
#487=VECTOR('',#7641,1.);
#488=VECTOR('',#7646,1.);
#489=VECTOR('',#7649,1.);
#490=VECTOR('',#7652,1.);
#491=VECTOR('',#7653,1.);
#492=VECTOR('',#7658,1.);
#493=VECTOR('',#7661,1.);
#494=VECTOR('',#7664,1.);
#495=VECTOR('',#7667,1.);
#496=VECTOR('',#7670,1.);
#497=VECTOR('',#7673,1.);
#498=VECTOR('',#7676,1.);
#499=VECTOR('',#7677,1.);
#500=VECTOR('',#7682,1.);
#501=VECTOR('',#7683,1.);
#502=VECTOR('',#7688,1.);
#503=VECTOR('',#7691,1.);
#504=VECTOR('',#7694,1.);
#505=VECTOR('',#7697,1.);
#506=VECTOR('',#7700,1.);
#507=VECTOR('',#7703,1.);
#508=VECTOR('',#7706,1.);
#509=VECTOR('',#7707,1.);
#510=VECTOR('',#7848,1.);
#511=VECTOR('',#7849,1.);
#512=VECTOR('',#7852,1.);
#513=VECTOR('',#7855,1.);
#514=VECTOR('',#7860,1.);
#515=VECTOR('',#7863,1.);
#516=VECTOR('',#7868,1.);
#517=VECTOR('',#7871,1.);
#518=VECTOR('',#7876,1.);
#519=VECTOR('',#7879,1.);
#520=VECTOR('',#7884,1.);
#521=VECTOR('',#7887,1.);
#522=VECTOR('',#7892,1.);
#523=VECTOR('',#7895,1.);
#524=VECTOR('',#7900,1.);
#525=VECTOR('',#7903,1.);
#526=VECTOR('',#7908,1.);
#527=VECTOR('',#7911,1.);
#528=VECTOR('',#7916,1.);
#529=VECTOR('',#7919,1.);
#530=VECTOR('',#7924,1.);
#531=VECTOR('',#7927,1.);
#532=VECTOR('',#7932,1.);
#533=VECTOR('',#7935,1.);
#534=VECTOR('',#7940,1.);
#535=VECTOR('',#7943,1.);
#536=VECTOR('',#7948,1.);
#537=VECTOR('',#7951,1.);
#538=VECTOR('',#7956,1.);
#539=VECTOR('',#7959,1.);
#540=VECTOR('',#7964,1.);
#541=VECTOR('',#7967,1.);
#542=VECTOR('',#7972,1.);
#543=VECTOR('',#7975,1.);
#544=VECTOR('',#7980,1.);
#545=VECTOR('',#7983,1.);
#546=VECTOR('',#7988,1.);
#547=VECTOR('',#7991,1.);
#548=VECTOR('',#7996,1.);
#549=VECTOR('',#7999,1.);
#550=VECTOR('',#8004,1.);
#551=VECTOR('',#8007,1.);
#552=VECTOR('',#8012,1.);
#553=VECTOR('',#8015,1.);
#554=VECTOR('',#8020,1.);
#555=VECTOR('',#8023,1.);
#678=SHAPE_REPRESENTATION_RELATIONSHIP('','',#5696,#692);
#692=ADVANCED_BREP_SHAPE_REPRESENTATION('',(#5665),#10150);
#757=PLANE('',#6080);
#758=PLANE('',#6211);
#759=PLANE('',#6346);
#760=PLANE('',#6349);
#761=PLANE('',#6352);
#762=PLANE('',#6356);
#763=PLANE('',#6359);
#1540=ORIENTED_EDGE('',*,*,#2707,.T.);
#1541=ORIENTED_EDGE('',*,*,#2708,.T.);
#1542=ORIENTED_EDGE('',*,*,#2709,.T.);
#1543=ORIENTED_EDGE('',*,*,#2710,.F.);
#1544=ORIENTED_EDGE('',*,*,#2711,.F.);
#1545=ORIENTED_EDGE('',*,*,#2712,.F.);
#1546=ORIENTED_EDGE('',*,*,#2713,.F.);
#1547=ORIENTED_EDGE('',*,*,#2714,.F.);
#1548=ORIENTED_EDGE('',*,*,#2715,.F.);
#1549=ORIENTED_EDGE('',*,*,#2716,.F.);
#1550=ORIENTED_EDGE('',*,*,#2717,.F.);
#1551=ORIENTED_EDGE('',*,*,#2718,.F.);
#1552=ORIENTED_EDGE('',*,*,#2719,.F.);
#1553=ORIENTED_EDGE('',*,*,#2720,.F.);
#1554=ORIENTED_EDGE('',*,*,#2721,.F.);
#1555=ORIENTED_EDGE('',*,*,#2722,.F.);
#1556=ORIENTED_EDGE('',*,*,#2723,.F.);
#1557=ORIENTED_EDGE('',*,*,#2724,.F.);
#1558=ORIENTED_EDGE('',*,*,#2725,.F.);
#1559=ORIENTED_EDGE('',*,*,#2726,.F.);
#1560=ORIENTED_EDGE('',*,*,#2727,.F.);
#1561=ORIENTED_EDGE('',*,*,#2728,.F.);
#1562=ORIENTED_EDGE('',*,*,#2729,.F.);
#1563=ORIENTED_EDGE('',*,*,#2730,.F.);
#1564=ORIENTED_EDGE('',*,*,#2731,.F.);
#1565=ORIENTED_EDGE('',*,*,#2732,.F.);
#1566=ORIENTED_EDGE('',*,*,#2733,.F.);
#1567=ORIENTED_EDGE('',*,*,#2734,.F.);
#1568=ORIENTED_EDGE('',*,*,#2735,.F.);
#1569=ORIENTED_EDGE('',*,*,#2736,.F.);
#1570=ORIENTED_EDGE('',*,*,#2737,.F.);
#1571=ORIENTED_EDGE('',*,*,#2738,.F.);
#1572=ORIENTED_EDGE('',*,*,#2739,.F.);
#1573=ORIENTED_EDGE('',*,*,#2740,.F.);
#1574=ORIENTED_EDGE('',*,*,#2741,.F.);
#1575=ORIENTED_EDGE('',*,*,#2742,.F.);
#1576=ORIENTED_EDGE('',*,*,#2743,.F.);
#1577=ORIENTED_EDGE('',*,*,#2744,.F.);
#1578=ORIENTED_EDGE('',*,*,#2745,.F.);
#1579=ORIENTED_EDGE('',*,*,#2746,.F.);
#1580=ORIENTED_EDGE('',*,*,#2747,.F.);
#1581=ORIENTED_EDGE('',*,*,#2748,.F.);
#1582=ORIENTED_EDGE('',*,*,#2749,.F.);
#1583=ORIENTED_EDGE('',*,*,#2750,.F.);
#1584=ORIENTED_EDGE('',*,*,#2751,.F.);
#1585=ORIENTED_EDGE('',*,*,#2752,.F.);
#1586=ORIENTED_EDGE('',*,*,#2753,.F.);
#1587=ORIENTED_EDGE('',*,*,#2754,.F.);
#1588=ORIENTED_EDGE('',*,*,#2755,.F.);
#1589=ORIENTED_EDGE('',*,*,#2756,.F.);
#1590=ORIENTED_EDGE('',*,*,#2757,.F.);
#1591=ORIENTED_EDGE('',*,*,#2758,.F.);
#1592=ORIENTED_EDGE('',*,*,#2759,.F.);
#1593=ORIENTED_EDGE('',*,*,#2760,.F.);
#1594=ORIENTED_EDGE('',*,*,#2761,.F.);
#1595=ORIENTED_EDGE('',*,*,#2762,.F.);
#1596=ORIENTED_EDGE('',*,*,#2763,.F.);
#1597=ORIENTED_EDGE('',*,*,#2764,.F.);
#1598=ORIENTED_EDGE('',*,*,#2765,.F.);
#1599=ORIENTED_EDGE('',*,*,#2766,.F.);
#1600=ORIENTED_EDGE('',*,*,#2767,.F.);
#1601=ORIENTED_EDGE('',*,*,#2768,.F.);
#1602=ORIENTED_EDGE('',*,*,#2769,.F.);
#1603=ORIENTED_EDGE('',*,*,#2770,.F.);
#1604=ORIENTED_EDGE('',*,*,#2771,.F.);
#1605=ORIENTED_EDGE('',*,*,#2772,.F.);
#1606=ORIENTED_EDGE('',*,*,#2773,.F.);
#1607=ORIENTED_EDGE('',*,*,#2774,.F.);
#1608=ORIENTED_EDGE('',*,*,#2775,.F.);
#1609=ORIENTED_EDGE('',*,*,#2776,.F.);
#1610=ORIENTED_EDGE('',*,*,#2777,.F.);
#1611=ORIENTED_EDGE('',*,*,#2778,.F.);
#1612=ORIENTED_EDGE('',*,*,#2779,.F.);
#1613=ORIENTED_EDGE('',*,*,#2780,.F.);
#1614=ORIENTED_EDGE('',*,*,#2781,.F.);
#1615=ORIENTED_EDGE('',*,*,#2782,.F.);
#1616=ORIENTED_EDGE('',*,*,#2783,.F.);
#1617=ORIENTED_EDGE('',*,*,#2784,.F.);
#1618=ORIENTED_EDGE('',*,*,#2785,.F.);
#1619=ORIENTED_EDGE('',*,*,#2786,.F.);
#1620=ORIENTED_EDGE('',*,*,#2787,.F.);
#1621=ORIENTED_EDGE('',*,*,#2788,.F.);
#1622=ORIENTED_EDGE('',*,*,#2789,.F.);
#1623=ORIENTED_EDGE('',*,*,#2790,.F.);
#1624=ORIENTED_EDGE('',*,*,#2791,.F.);
#1625=ORIENTED_EDGE('',*,*,#2792,.F.);
#1626=ORIENTED_EDGE('',*,*,#2793,.F.);
#1627=ORIENTED_EDGE('',*,*,#2794,.F.);
#1628=ORIENTED_EDGE('',*,*,#2795,.F.);
#1629=ORIENTED_EDGE('',*,*,#2796,.F.);
#1630=ORIENTED_EDGE('',*,*,#2797,.F.);
#1631=ORIENTED_EDGE('',*,*,#2798,.F.);
#1632=ORIENTED_EDGE('',*,*,#2709,.F.);
#1633=ORIENTED_EDGE('',*,*,#2799,.F.);
#1634=ORIENTED_EDGE('',*,*,#2798,.T.);
#1635=ORIENTED_EDGE('',*,*,#2800,.F.);
#1636=ORIENTED_EDGE('',*,*,#2801,.F.);
#1637=ORIENTED_EDGE('',*,*,#2802,.F.);
#1638=ORIENTED_EDGE('',*,*,#2803,.F.);
#1639=ORIENTED_EDGE('',*,*,#2804,.F.);
#1640=ORIENTED_EDGE('',*,*,#2714,.T.);
#1641=ORIENTED_EDGE('',*,*,#2805,.F.);
#1642=ORIENTED_EDGE('',*,*,#2794,.T.);
#1643=ORIENTED_EDGE('',*,*,#2806,.F.);
#1644=ORIENTED_EDGE('',*,*,#2807,.F.);
#1645=ORIENTED_EDGE('',*,*,#2808,.F.);
#1646=ORIENTED_EDGE('',*,*,#2790,.T.);
#1647=ORIENTED_EDGE('',*,*,#2809,.F.);
#1648=ORIENTED_EDGE('',*,*,#2810,.F.);
#1649=ORIENTED_EDGE('',*,*,#2811,.F.);
#1650=ORIENTED_EDGE('',*,*,#2782,.T.);
#1651=ORIENTED_EDGE('',*,*,#2812,.F.);
#1652=ORIENTED_EDGE('',*,*,#2813,.F.);
#1653=ORIENTED_EDGE('',*,*,#2814,.F.);
#1654=ORIENTED_EDGE('',*,*,#2815,.F.);
#1655=ORIENTED_EDGE('',*,*,#2816,.F.);
#1656=ORIENTED_EDGE('',*,*,#2786,.T.);
#1657=ORIENTED_EDGE('',*,*,#2817,.F.);
#1658=ORIENTED_EDGE('',*,*,#2730,.T.);
#1659=ORIENTED_EDGE('',*,*,#2818,.F.);
#1660=ORIENTED_EDGE('',*,*,#2819,.F.);
#1661=ORIENTED_EDGE('',*,*,#2820,.F.);
#1662=ORIENTED_EDGE('',*,*,#2821,.F.);
#1663=ORIENTED_EDGE('',*,*,#2822,.F.);
#1664=ORIENTED_EDGE('',*,*,#2734,.T.);
#1665=ORIENTED_EDGE('',*,*,#2823,.F.);
#1666=ORIENTED_EDGE('',*,*,#2726,.T.);
#1667=ORIENTED_EDGE('',*,*,#2824,.F.);
#1668=ORIENTED_EDGE('',*,*,#2825,.F.);
#1669=ORIENTED_EDGE('',*,*,#2826,.F.);
#1670=ORIENTED_EDGE('',*,*,#2722,.T.);
#1671=ORIENTED_EDGE('',*,*,#2827,.F.);
#1672=ORIENTED_EDGE('',*,*,#2828,.F.);
#1673=ORIENTED_EDGE('',*,*,#2829,.F.);
#1674=ORIENTED_EDGE('',*,*,#2830,.F.);
#1675=ORIENTED_EDGE('',*,*,#2831,.F.);
#1676=ORIENTED_EDGE('',*,*,#2718,.T.);
#1677=ORIENTED_EDGE('',*,*,#2832,.F.);
#1678=ORIENTED_EDGE('',*,*,#2742,.T.);
#1679=ORIENTED_EDGE('',*,*,#2833,.F.);
#1680=ORIENTED_EDGE('',*,*,#2834,.F.);
#1681=ORIENTED_EDGE('',*,*,#2835,.F.);
#1682=ORIENTED_EDGE('',*,*,#2836,.F.);
#1683=ORIENTED_EDGE('',*,*,#2837,.F.);
#1684=ORIENTED_EDGE('',*,*,#2746,.T.);
#1685=ORIENTED_EDGE('',*,*,#2838,.F.);
#1686=ORIENTED_EDGE('',*,*,#2839,.F.);
#1687=ORIENTED_EDGE('',*,*,#2840,.F.);
#1688=ORIENTED_EDGE('',*,*,#2750,.T.);
#1689=ORIENTED_EDGE('',*,*,#2841,.F.);
#1690=ORIENTED_EDGE('',*,*,#2842,.F.);
#1691=ORIENTED_EDGE('',*,*,#2843,.F.);
#1692=ORIENTED_EDGE('',*,*,#2754,.T.);
#1693=ORIENTED_EDGE('',*,*,#2844,.F.);
#1694=ORIENTED_EDGE('',*,*,#2738,.T.);
#1695=ORIENTED_EDGE('',*,*,#2845,.F.);
#1696=ORIENTED_EDGE('',*,*,#2846,.F.);
#1697=ORIENTED_EDGE('',*,*,#2847,.F.);
#1698=ORIENTED_EDGE('',*,*,#2762,.T.);
#1699=ORIENTED_EDGE('',*,*,#2848,.F.);
#1700=ORIENTED_EDGE('',*,*,#2849,.F.);
#1701=ORIENTED_EDGE('',*,*,#2850,.F.);
#1702=ORIENTED_EDGE('',*,*,#2851,.F.);
#1703=ORIENTED_EDGE('',*,*,#2852,.F.);
#1704=ORIENTED_EDGE('',*,*,#2766,.T.);
#1705=ORIENTED_EDGE('',*,*,#2853,.F.);
#1706=ORIENTED_EDGE('',*,*,#2854,.F.);
#1707=ORIENTED_EDGE('',*,*,#2855,.F.);
#1708=ORIENTED_EDGE('',*,*,#2770,.T.);
#1709=ORIENTED_EDGE('',*,*,#2856,.F.);
#1710=ORIENTED_EDGE('',*,*,#2857,.F.);
#1711=ORIENTED_EDGE('',*,*,#2858,.F.);
#1712=ORIENTED_EDGE('',*,*,#2774,.T.);
#1713=ORIENTED_EDGE('',*,*,#2859,.F.);
#1714=ORIENTED_EDGE('',*,*,#2758,.T.);
#1715=ORIENTED_EDGE('',*,*,#2860,.F.);
#1716=ORIENTED_EDGE('',*,*,#2861,.F.);
#1717=ORIENTED_EDGE('',*,*,#2707,.F.);
#1718=ORIENTED_EDGE('',*,*,#2862,.T.);
#1719=ORIENTED_EDGE('',*,*,#2801,.T.);
#1720=ORIENTED_EDGE('',*,*,#2863,.F.);
#1721=ORIENTED_EDGE('',*,*,#2864,.T.);
#1722=ORIENTED_EDGE('',*,*,#2865,.T.);
#1723=ORIENTED_EDGE('',*,*,#2807,.T.);
#1724=ORIENTED_EDGE('',*,*,#2866,.F.);
#1725=ORIENTED_EDGE('',*,*,#2867,.T.);
#1726=ORIENTED_EDGE('',*,*,#2868,.T.);
#1727=ORIENTED_EDGE('',*,*,#2810,.T.);
#1728=ORIENTED_EDGE('',*,*,#2869,.F.);
#1729=ORIENTED_EDGE('',*,*,#2870,.T.);
#1730=ORIENTED_EDGE('',*,*,#2871,.T.);
#1731=ORIENTED_EDGE('',*,*,#2815,.T.);
#1732=ORIENTED_EDGE('',*,*,#2872,.F.);
#1733=ORIENTED_EDGE('',*,*,#2873,.T.);
#1734=ORIENTED_EDGE('',*,*,#2874,.T.);
#1735=ORIENTED_EDGE('',*,*,#2813,.T.);
#1736=ORIENTED_EDGE('',*,*,#2875,.F.);
#1737=ORIENTED_EDGE('',*,*,#2876,.T.);
#1738=ORIENTED_EDGE('',*,*,#2877,.T.);
#1739=ORIENTED_EDGE('',*,*,#2878,.T.);
#1740=ORIENTED_EDGE('',*,*,#2879,.F.);
#1741=ORIENTED_EDGE('',*,*,#2880,.T.);
#1742=ORIENTED_EDGE('',*,*,#2881,.T.);
#1743=ORIENTED_EDGE('',*,*,#2857,.T.);
#1744=ORIENTED_EDGE('',*,*,#2882,.F.);
#1745=ORIENTED_EDGE('',*,*,#2883,.T.);
#1746=ORIENTED_EDGE('',*,*,#2884,.T.);
#1747=ORIENTED_EDGE('',*,*,#2854,.T.);
#1748=ORIENTED_EDGE('',*,*,#2885,.F.);
#1749=ORIENTED_EDGE('',*,*,#2886,.T.);
#1750=ORIENTED_EDGE('',*,*,#2887,.T.);
#1751=ORIENTED_EDGE('',*,*,#2851,.T.);
#1752=ORIENTED_EDGE('',*,*,#2888,.F.);
#1753=ORIENTED_EDGE('',*,*,#2889,.T.);
#1754=ORIENTED_EDGE('',*,*,#2890,.T.);
#1755=ORIENTED_EDGE('',*,*,#2849,.T.);
#1756=ORIENTED_EDGE('',*,*,#2891,.F.);
#1757=ORIENTED_EDGE('',*,*,#2892,.T.);
#1758=ORIENTED_EDGE('',*,*,#2893,.T.);
#1759=ORIENTED_EDGE('',*,*,#2861,.T.);
#1760=ORIENTED_EDGE('',*,*,#2894,.F.);
#1761=ORIENTED_EDGE('',*,*,#2895,.T.);
#1762=ORIENTED_EDGE('',*,*,#2896,.T.);
#1763=ORIENTED_EDGE('',*,*,#2842,.T.);
#1764=ORIENTED_EDGE('',*,*,#2897,.F.);
#1765=ORIENTED_EDGE('',*,*,#2898,.T.);
#1766=ORIENTED_EDGE('',*,*,#2899,.T.);
#1767=ORIENTED_EDGE('',*,*,#2839,.T.);
#1768=ORIENTED_EDGE('',*,*,#2900,.F.);
#1769=ORIENTED_EDGE('',*,*,#2901,.T.);
#1770=ORIENTED_EDGE('',*,*,#2902,.T.);
#1771=ORIENTED_EDGE('',*,*,#2836,.T.);
#1772=ORIENTED_EDGE('',*,*,#2903,.F.);
#1773=ORIENTED_EDGE('',*,*,#2904,.T.);
#1774=ORIENTED_EDGE('',*,*,#2905,.T.);
#1775=ORIENTED_EDGE('',*,*,#2834,.T.);
#1776=ORIENTED_EDGE('',*,*,#2906,.F.);
#1777=ORIENTED_EDGE('',*,*,#2907,.T.);
#1778=ORIENTED_EDGE('',*,*,#2908,.T.);
#1779=ORIENTED_EDGE('',*,*,#2846,.T.);
#1780=ORIENTED_EDGE('',*,*,#2909,.F.);
#1781=ORIENTED_EDGE('',*,*,#2910,.T.);
#1782=ORIENTED_EDGE('',*,*,#2911,.T.);
#1783=ORIENTED_EDGE('',*,*,#2821,.T.);
#1784=ORIENTED_EDGE('',*,*,#2912,.F.);
#1785=ORIENTED_EDGE('',*,*,#2913,.T.);
#1786=ORIENTED_EDGE('',*,*,#2914,.T.);
#1787=ORIENTED_EDGE('',*,*,#2819,.T.);
#1788=ORIENTED_EDGE('',*,*,#2915,.F.);
#1789=ORIENTED_EDGE('',*,*,#2916,.T.);
#1790=ORIENTED_EDGE('',*,*,#2917,.T.);
#1791=ORIENTED_EDGE('',*,*,#2825,.T.);
#1792=ORIENTED_EDGE('',*,*,#2918,.F.);
#1793=ORIENTED_EDGE('',*,*,#2919,.T.);
#1794=ORIENTED_EDGE('',*,*,#2920,.T.);
#1795=ORIENTED_EDGE('',*,*,#2828,.T.);
#1796=ORIENTED_EDGE('',*,*,#2921,.F.);
#1797=ORIENTED_EDGE('',*,*,#2922,.T.);
#1798=ORIENTED_EDGE('',*,*,#2923,.T.);
#1799=ORIENTED_EDGE('',*,*,#2830,.T.);
#1800=ORIENTED_EDGE('',*,*,#2924,.F.);
#1801=ORIENTED_EDGE('',*,*,#2925,.T.);
#1802=ORIENTED_EDGE('',*,*,#2926,.T.);
#1803=ORIENTED_EDGE('',*,*,#2803,.T.);
#1804=ORIENTED_EDGE('',*,*,#2927,.F.);
#1805=ORIENTED_EDGE('',*,*,#2928,.T.);
#1806=ORIENTED_EDGE('',*,*,#2929,.F.);
#1807=ORIENTED_EDGE('',*,*,#2778,.T.);
#1808=ORIENTED_EDGE('',*,*,#2930,.F.);
#1809=ORIENTED_EDGE('',*,*,#2878,.F.);
#1810=ORIENTED_EDGE('',*,*,#2858,.T.);
#1811=ORIENTED_EDGE('',*,*,#2881,.F.);
#1812=ORIENTED_EDGE('',*,*,#2931,.F.);
#1813=ORIENTED_EDGE('',*,*,#2775,.T.);
#1814=ORIENTED_EDGE('',*,*,#2930,.T.);
#1815=ORIENTED_EDGE('',*,*,#2777,.T.);
#1816=ORIENTED_EDGE('',*,*,#2932,.T.);
#1817=ORIENTED_EDGE('',*,*,#2879,.T.);
#1818=ORIENTED_EDGE('',*,*,#2880,.F.);
#1819=ORIENTED_EDGE('',*,*,#2932,.F.);
#1820=ORIENTED_EDGE('',*,*,#2776,.T.);
#1821=ORIENTED_EDGE('',*,*,#2931,.T.);
#1822=ORIENTED_EDGE('',*,*,#2929,.T.);
#1823=ORIENTED_EDGE('',*,*,#2877,.F.);
#1824=ORIENTED_EDGE('',*,*,#2933,.F.);
#1825=ORIENTED_EDGE('',*,*,#2779,.T.);
#1826=ORIENTED_EDGE('',*,*,#2812,.T.);
#1827=ORIENTED_EDGE('',*,*,#2781,.T.);
#1828=ORIENTED_EDGE('',*,*,#2934,.T.);
#1829=ORIENTED_EDGE('',*,*,#2875,.T.);
#1830=ORIENTED_EDGE('',*,*,#2876,.F.);
#1831=ORIENTED_EDGE('',*,*,#2934,.F.);
#1832=ORIENTED_EDGE('',*,*,#2780,.T.);
#1833=ORIENTED_EDGE('',*,*,#2933,.T.);
#1834=ORIENTED_EDGE('',*,*,#2843,.T.);
#1835=ORIENTED_EDGE('',*,*,#2896,.F.);
#1836=ORIENTED_EDGE('',*,*,#2935,.F.);
#1837=ORIENTED_EDGE('',*,*,#2755,.T.);
#1838=ORIENTED_EDGE('',*,*,#2860,.T.);
#1839=ORIENTED_EDGE('',*,*,#2757,.T.);
#1840=ORIENTED_EDGE('',*,*,#2936,.T.);
#1841=ORIENTED_EDGE('',*,*,#2894,.T.);
#1842=ORIENTED_EDGE('',*,*,#2895,.F.);
#1843=ORIENTED_EDGE('',*,*,#2936,.F.);
#1844=ORIENTED_EDGE('',*,*,#2756,.T.);
#1845=ORIENTED_EDGE('',*,*,#2935,.T.);
#1846=ORIENTED_EDGE('',*,*,#2859,.T.);
#1847=ORIENTED_EDGE('',*,*,#2893,.F.);
#1848=ORIENTED_EDGE('',*,*,#2937,.F.);
#1849=ORIENTED_EDGE('',*,*,#2759,.T.);
#1850=ORIENTED_EDGE('',*,*,#2848,.T.);
#1851=ORIENTED_EDGE('',*,*,#2761,.T.);
#1852=ORIENTED_EDGE('',*,*,#2938,.T.);
#1853=ORIENTED_EDGE('',*,*,#2891,.T.);
#1854=ORIENTED_EDGE('',*,*,#2892,.F.);
#1855=ORIENTED_EDGE('',*,*,#2938,.F.);
#1856=ORIENTED_EDGE('',*,*,#2760,.T.);
#1857=ORIENTED_EDGE('',*,*,#2937,.T.);
#1858=ORIENTED_EDGE('',*,*,#2855,.T.);
#1859=ORIENTED_EDGE('',*,*,#2884,.F.);
#1860=ORIENTED_EDGE('',*,*,#2939,.F.);
#1861=ORIENTED_EDGE('',*,*,#2771,.T.);
#1862=ORIENTED_EDGE('',*,*,#2856,.T.);
#1863=ORIENTED_EDGE('',*,*,#2773,.T.);
#1864=ORIENTED_EDGE('',*,*,#2940,.T.);
#1865=ORIENTED_EDGE('',*,*,#2882,.T.);
#1866=ORIENTED_EDGE('',*,*,#2883,.F.);
#1867=ORIENTED_EDGE('',*,*,#2940,.F.);
#1868=ORIENTED_EDGE('',*,*,#2772,.T.);
#1869=ORIENTED_EDGE('',*,*,#2939,.T.);
#1870=ORIENTED_EDGE('',*,*,#2852,.T.);
#1871=ORIENTED_EDGE('',*,*,#2887,.F.);
#1872=ORIENTED_EDGE('',*,*,#2941,.F.);
#1873=ORIENTED_EDGE('',*,*,#2767,.T.);
#1874=ORIENTED_EDGE('',*,*,#2853,.T.);
#1875=ORIENTED_EDGE('',*,*,#2769,.T.);
#1876=ORIENTED_EDGE('',*,*,#2942,.T.);
#1877=ORIENTED_EDGE('',*,*,#2885,.T.);
#1878=ORIENTED_EDGE('',*,*,#2886,.F.);
#1879=ORIENTED_EDGE('',*,*,#2942,.F.);
#1880=ORIENTED_EDGE('',*,*,#2768,.T.);
#1881=ORIENTED_EDGE('',*,*,#2941,.T.);
#1882=ORIENTED_EDGE('',*,*,#2847,.T.);
#1883=ORIENTED_EDGE('',*,*,#2890,.F.);
#1884=ORIENTED_EDGE('',*,*,#2943,.F.);
#1885=ORIENTED_EDGE('',*,*,#2763,.T.);
#1886=ORIENTED_EDGE('',*,*,#2850,.T.);
#1887=ORIENTED_EDGE('',*,*,#2765,.T.);
#1888=ORIENTED_EDGE('',*,*,#2944,.T.);
#1889=ORIENTED_EDGE('',*,*,#2888,.T.);
#1890=ORIENTED_EDGE('',*,*,#2889,.F.);
#1891=ORIENTED_EDGE('',*,*,#2944,.F.);
#1892=ORIENTED_EDGE('',*,*,#2764,.T.);
#1893=ORIENTED_EDGE('',*,*,#2943,.T.);
#1894=ORIENTED_EDGE('',*,*,#2822,.T.);
#1895=ORIENTED_EDGE('',*,*,#2911,.F.);
#1896=ORIENTED_EDGE('',*,*,#2945,.F.);
#1897=ORIENTED_EDGE('',*,*,#2735,.T.);
#1898=ORIENTED_EDGE('',*,*,#2845,.T.);
#1899=ORIENTED_EDGE('',*,*,#2737,.T.);
#1900=ORIENTED_EDGE('',*,*,#2946,.T.);
#1901=ORIENTED_EDGE('',*,*,#2909,.T.);
#1902=ORIENTED_EDGE('',*,*,#2910,.F.);
#1903=ORIENTED_EDGE('',*,*,#2946,.F.);
#1904=ORIENTED_EDGE('',*,*,#2736,.T.);
#1905=ORIENTED_EDGE('',*,*,#2945,.T.);
#1906=ORIENTED_EDGE('',*,*,#2844,.T.);
#1907=ORIENTED_EDGE('',*,*,#2908,.F.);
#1908=ORIENTED_EDGE('',*,*,#2947,.F.);
#1909=ORIENTED_EDGE('',*,*,#2739,.T.);
#1910=ORIENTED_EDGE('',*,*,#2833,.T.);
#1911=ORIENTED_EDGE('',*,*,#2741,.T.);
#1912=ORIENTED_EDGE('',*,*,#2948,.T.);
#1913=ORIENTED_EDGE('',*,*,#2906,.T.);
#1914=ORIENTED_EDGE('',*,*,#2907,.F.);
#1915=ORIENTED_EDGE('',*,*,#2948,.F.);
#1916=ORIENTED_EDGE('',*,*,#2740,.T.);
#1917=ORIENTED_EDGE('',*,*,#2947,.T.);
#1918=ORIENTED_EDGE('',*,*,#2840,.T.);
#1919=ORIENTED_EDGE('',*,*,#2899,.F.);
#1920=ORIENTED_EDGE('',*,*,#2949,.F.);
#1921=ORIENTED_EDGE('',*,*,#2751,.T.);
#1922=ORIENTED_EDGE('',*,*,#2841,.T.);
#1923=ORIENTED_EDGE('',*,*,#2753,.T.);
#1924=ORIENTED_EDGE('',*,*,#2950,.T.);
#1925=ORIENTED_EDGE('',*,*,#2897,.T.);
#1926=ORIENTED_EDGE('',*,*,#2898,.F.);
#1927=ORIENTED_EDGE('',*,*,#2950,.F.);
#1928=ORIENTED_EDGE('',*,*,#2752,.T.);
#1929=ORIENTED_EDGE('',*,*,#2949,.T.);
#1930=ORIENTED_EDGE('',*,*,#2837,.T.);
#1931=ORIENTED_EDGE('',*,*,#2902,.F.);
#1932=ORIENTED_EDGE('',*,*,#2951,.F.);
#1933=ORIENTED_EDGE('',*,*,#2747,.T.);
#1934=ORIENTED_EDGE('',*,*,#2838,.T.);
#1935=ORIENTED_EDGE('',*,*,#2749,.T.);
#1936=ORIENTED_EDGE('',*,*,#2952,.T.);
#1937=ORIENTED_EDGE('',*,*,#2900,.T.);
#1938=ORIENTED_EDGE('',*,*,#2901,.F.);
#1939=ORIENTED_EDGE('',*,*,#2952,.F.);
#1940=ORIENTED_EDGE('',*,*,#2748,.T.);
#1941=ORIENTED_EDGE('',*,*,#2951,.T.);
#1942=ORIENTED_EDGE('',*,*,#2832,.T.);
#1943=ORIENTED_EDGE('',*,*,#2905,.F.);
#1944=ORIENTED_EDGE('',*,*,#2953,.F.);
#1945=ORIENTED_EDGE('',*,*,#2743,.T.);
#1946=ORIENTED_EDGE('',*,*,#2835,.T.);
#1947=ORIENTED_EDGE('',*,*,#2745,.T.);
#1948=ORIENTED_EDGE('',*,*,#2954,.T.);
#1949=ORIENTED_EDGE('',*,*,#2903,.T.);
#1950=ORIENTED_EDGE('',*,*,#2904,.F.);
#1951=ORIENTED_EDGE('',*,*,#2954,.F.);
#1952=ORIENTED_EDGE('',*,*,#2744,.T.);
#1953=ORIENTED_EDGE('',*,*,#2953,.T.);
#1954=ORIENTED_EDGE('',*,*,#2831,.T.);
#1955=ORIENTED_EDGE('',*,*,#2923,.F.);
#1956=ORIENTED_EDGE('',*,*,#2955,.F.);
#1957=ORIENTED_EDGE('',*,*,#2719,.T.);
#1958=ORIENTED_EDGE('',*,*,#2827,.T.);
#1959=ORIENTED_EDGE('',*,*,#2721,.T.);
#1960=ORIENTED_EDGE('',*,*,#2956,.T.);
#1961=ORIENTED_EDGE('',*,*,#2921,.T.);
#1962=ORIENTED_EDGE('',*,*,#2922,.F.);
#1963=ORIENTED_EDGE('',*,*,#2956,.F.);
#1964=ORIENTED_EDGE('',*,*,#2720,.T.);
#1965=ORIENTED_EDGE('',*,*,#2955,.T.);
#1966=ORIENTED_EDGE('',*,*,#2804,.T.);
#1967=ORIENTED_EDGE('',*,*,#2926,.F.);
#1968=ORIENTED_EDGE('',*,*,#2957,.F.);
#1969=ORIENTED_EDGE('',*,*,#2715,.T.);
#1970=ORIENTED_EDGE('',*,*,#2829,.T.);
#1971=ORIENTED_EDGE('',*,*,#2717,.T.);
#1972=ORIENTED_EDGE('',*,*,#2958,.T.);
#1973=ORIENTED_EDGE('',*,*,#2924,.T.);
#1974=ORIENTED_EDGE('',*,*,#2925,.F.);
#1975=ORIENTED_EDGE('',*,*,#2958,.F.);
#1976=ORIENTED_EDGE('',*,*,#2716,.T.);
#1977=ORIENTED_EDGE('',*,*,#2957,.T.);
#1978=ORIENTED_EDGE('',*,*,#2826,.T.);
#1979=ORIENTED_EDGE('',*,*,#2920,.F.);
#1980=ORIENTED_EDGE('',*,*,#2959,.F.);
#1981=ORIENTED_EDGE('',*,*,#2723,.T.);
#1982=ORIENTED_EDGE('',*,*,#2824,.T.);
#1983=ORIENTED_EDGE('',*,*,#2725,.T.);
#1984=ORIENTED_EDGE('',*,*,#2960,.T.);
#1985=ORIENTED_EDGE('',*,*,#2918,.T.);
#1986=ORIENTED_EDGE('',*,*,#2919,.F.);
#1987=ORIENTED_EDGE('',*,*,#2960,.F.);
#1988=ORIENTED_EDGE('',*,*,#2724,.T.);
#1989=ORIENTED_EDGE('',*,*,#2959,.T.);
#1990=ORIENTED_EDGE('',*,*,#2823,.T.);
#1991=ORIENTED_EDGE('',*,*,#2917,.F.);
#1992=ORIENTED_EDGE('',*,*,#2961,.F.);
#1993=ORIENTED_EDGE('',*,*,#2727,.T.);
#1994=ORIENTED_EDGE('',*,*,#2818,.T.);
#1995=ORIENTED_EDGE('',*,*,#2729,.T.);
#1996=ORIENTED_EDGE('',*,*,#2962,.T.);
#1997=ORIENTED_EDGE('',*,*,#2915,.T.);
#1998=ORIENTED_EDGE('',*,*,#2916,.F.);
#1999=ORIENTED_EDGE('',*,*,#2962,.F.);
#2000=ORIENTED_EDGE('',*,*,#2728,.T.);
#2001=ORIENTED_EDGE('',*,*,#2961,.T.);
#2002=ORIENTED_EDGE('',*,*,#2817,.T.);
#2003=ORIENTED_EDGE('',*,*,#2914,.F.);
#2004=ORIENTED_EDGE('',*,*,#2963,.F.);
#2005=ORIENTED_EDGE('',*,*,#2731,.T.);
#2006=ORIENTED_EDGE('',*,*,#2820,.T.);
#2007=ORIENTED_EDGE('',*,*,#2733,.T.);
#2008=ORIENTED_EDGE('',*,*,#2964,.T.);
#2009=ORIENTED_EDGE('',*,*,#2912,.T.);
#2010=ORIENTED_EDGE('',*,*,#2913,.F.);
#2011=ORIENTED_EDGE('',*,*,#2964,.F.);
#2012=ORIENTED_EDGE('',*,*,#2732,.T.);
#2013=ORIENTED_EDGE('',*,*,#2963,.T.);
#2014=ORIENTED_EDGE('',*,*,#2816,.T.);
#2015=ORIENTED_EDGE('',*,*,#2871,.F.);
#2016=ORIENTED_EDGE('',*,*,#2965,.F.);
#2017=ORIENTED_EDGE('',*,*,#2787,.T.);
#2018=ORIENTED_EDGE('',*,*,#2809,.T.);
#2019=ORIENTED_EDGE('',*,*,#2789,.T.);
#2020=ORIENTED_EDGE('',*,*,#2966,.T.);
#2021=ORIENTED_EDGE('',*,*,#2869,.T.);
#2022=ORIENTED_EDGE('',*,*,#2870,.F.);
#2023=ORIENTED_EDGE('',*,*,#2966,.F.);
#2024=ORIENTED_EDGE('',*,*,#2788,.T.);
#2025=ORIENTED_EDGE('',*,*,#2965,.T.);
#2026=ORIENTED_EDGE('',*,*,#2811,.T.);
#2027=ORIENTED_EDGE('',*,*,#2874,.F.);
#2028=ORIENTED_EDGE('',*,*,#2967,.F.);
#2029=ORIENTED_EDGE('',*,*,#2783,.T.);
#2030=ORIENTED_EDGE('',*,*,#2814,.T.);
#2031=ORIENTED_EDGE('',*,*,#2785,.T.);
#2032=ORIENTED_EDGE('',*,*,#2968,.T.);
#2033=ORIENTED_EDGE('',*,*,#2872,.T.);
#2034=ORIENTED_EDGE('',*,*,#2873,.F.);
#2035=ORIENTED_EDGE('',*,*,#2968,.F.);
#2036=ORIENTED_EDGE('',*,*,#2784,.T.);
#2037=ORIENTED_EDGE('',*,*,#2967,.T.);
#2038=ORIENTED_EDGE('',*,*,#2808,.T.);
#2039=ORIENTED_EDGE('',*,*,#2868,.F.);
#2040=ORIENTED_EDGE('',*,*,#2969,.F.);
#2041=ORIENTED_EDGE('',*,*,#2791,.T.);
#2042=ORIENTED_EDGE('',*,*,#2806,.T.);
#2043=ORIENTED_EDGE('',*,*,#2793,.T.);
#2044=ORIENTED_EDGE('',*,*,#2970,.T.);
#2045=ORIENTED_EDGE('',*,*,#2866,.T.);
#2046=ORIENTED_EDGE('',*,*,#2867,.F.);
#2047=ORIENTED_EDGE('',*,*,#2970,.F.);
#2048=ORIENTED_EDGE('',*,*,#2792,.T.);
#2049=ORIENTED_EDGE('',*,*,#2969,.T.);
#2050=ORIENTED_EDGE('',*,*,#2805,.T.);
#2051=ORIENTED_EDGE('',*,*,#2865,.F.);
#2052=ORIENTED_EDGE('',*,*,#2971,.F.);
#2053=ORIENTED_EDGE('',*,*,#2795,.T.);
#2054=ORIENTED_EDGE('',*,*,#2800,.T.);
#2055=ORIENTED_EDGE('',*,*,#2797,.T.);
#2056=ORIENTED_EDGE('',*,*,#2972,.T.);
#2057=ORIENTED_EDGE('',*,*,#2863,.T.);
#2058=ORIENTED_EDGE('',*,*,#2864,.F.);
#2059=ORIENTED_EDGE('',*,*,#2972,.F.);
#2060=ORIENTED_EDGE('',*,*,#2796,.T.);
#2061=ORIENTED_EDGE('',*,*,#2971,.T.);
#2062=ORIENTED_EDGE('',*,*,#2799,.T.);
#2063=ORIENTED_EDGE('',*,*,#2862,.F.);
#2064=ORIENTED_EDGE('',*,*,#2973,.F.);
#2065=ORIENTED_EDGE('',*,*,#2711,.T.);
#2066=ORIENTED_EDGE('',*,*,#2802,.T.);
#2067=ORIENTED_EDGE('',*,*,#2713,.T.);
#2068=ORIENTED_EDGE('',*,*,#2974,.T.);
#2069=ORIENTED_EDGE('',*,*,#2927,.T.);
#2070=ORIENTED_EDGE('',*,*,#2928,.F.);
#2071=ORIENTED_EDGE('',*,*,#2974,.F.);
#2072=ORIENTED_EDGE('',*,*,#2712,.T.);
#2073=ORIENTED_EDGE('',*,*,#2973,.T.);
#2074=ORIENTED_EDGE('',*,*,#2975,.F.);
#2075=ORIENTED_EDGE('',*,*,#2976,.T.);
#2076=ORIENTED_EDGE('',*,*,#2710,.T.);
#2077=ORIENTED_EDGE('',*,*,#2977,.F.);
#2078=ORIENTED_EDGE('',*,*,#2977,.T.);
#2079=ORIENTED_EDGE('',*,*,#2976,.F.);
#2080=ORIENTED_EDGE('',*,*,#2708,.F.);
#2081=ORIENTED_EDGE('',*,*,#2978,.F.);
#2082=ORIENTED_EDGE('',*,*,#2979,.T.);
#2083=ORIENTED_EDGE('',*,*,#2980,.T.);
#2084=ORIENTED_EDGE('',*,*,#2979,.F.);
#2085=ORIENTED_EDGE('',*,*,#2975,.T.);
#2086=ORIENTED_EDGE('',*,*,#2980,.F.);
#2087=ORIENTED_EDGE('',*,*,#2978,.T.);
#2707=EDGE_CURVE('',#3369,#3369,#3852,.F.);
#2708=EDGE_CURVE('',#3370,#3370,#3853,.T.);
#2709=EDGE_CURVE('',#3371,#3371,#3854,.F.);
#2710=EDGE_CURVE('',#3372,#3372,#3855,.T.);
#2711=EDGE_CURVE('',#3373,#3374,#3856,.T.);
#2712=EDGE_CURVE('',#3375,#3373,#3857,.T.);
#2713=EDGE_CURVE('',#3376,#3375,#3858,.T.);
#2714=EDGE_CURVE('',#3377,#3376,#3859,.T.);
#2715=EDGE_CURVE('',#3378,#3377,#3860,.T.);
#2716=EDGE_CURVE('',#3379,#3378,#3861,.T.);
#2717=EDGE_CURVE('',#3380,#3379,#3862,.T.);
#2718=EDGE_CURVE('',#3381,#3380,#3863,.T.);
#2719=EDGE_CURVE('',#3382,#3381,#3864,.T.);
#2720=EDGE_CURVE('',#3383,#3382,#3865,.T.);
#2721=EDGE_CURVE('',#3384,#3383,#3866,.T.);
#2722=EDGE_CURVE('',#3385,#3384,#3867,.T.);
#2723=EDGE_CURVE('',#3386,#3385,#3868,.T.);
#2724=EDGE_CURVE('',#3387,#3386,#3869,.T.);
#2725=EDGE_CURVE('',#3388,#3387,#3870,.T.);
#2726=EDGE_CURVE('',#3389,#3388,#3871,.T.);
#2727=EDGE_CURVE('',#3390,#3389,#3872,.T.);
#2728=EDGE_CURVE('',#3391,#3390,#3873,.T.);
#2729=EDGE_CURVE('',#3392,#3391,#3874,.T.);
#2730=EDGE_CURVE('',#3393,#3392,#3875,.T.);
#2731=EDGE_CURVE('',#3394,#3393,#3876,.T.);
#2732=EDGE_CURVE('',#3395,#3394,#3877,.T.);
#2733=EDGE_CURVE('',#3396,#3395,#3878,.T.);
#2734=EDGE_CURVE('',#3397,#3396,#3879,.T.);
#2735=EDGE_CURVE('',#3398,#3397,#3880,.T.);
#2736=EDGE_CURVE('',#3399,#3398,#3881,.T.);
#2737=EDGE_CURVE('',#3400,#3399,#3882,.T.);
#2738=EDGE_CURVE('',#3401,#3400,#3883,.T.);
#2739=EDGE_CURVE('',#3402,#3401,#3884,.T.);
#2740=EDGE_CURVE('',#3403,#3402,#3885,.T.);
#2741=EDGE_CURVE('',#3404,#3403,#3886,.T.);
#2742=EDGE_CURVE('',#3405,#3404,#3887,.T.);
#2743=EDGE_CURVE('',#3406,#3405,#3888,.T.);
#2744=EDGE_CURVE('',#3407,#3406,#3889,.T.);
#2745=EDGE_CURVE('',#3408,#3407,#3890,.T.);
#2746=EDGE_CURVE('',#3409,#3408,#3891,.T.);
#2747=EDGE_CURVE('',#3410,#3409,#3892,.T.);
#2748=EDGE_CURVE('',#3411,#3410,#3893,.T.);
#2749=EDGE_CURVE('',#3412,#3411,#3894,.T.);
#2750=EDGE_CURVE('',#3413,#3412,#3895,.T.);
#2751=EDGE_CURVE('',#3414,#3413,#3896,.T.);
#2752=EDGE_CURVE('',#3415,#3414,#3897,.T.);
#2753=EDGE_CURVE('',#3416,#3415,#3898,.T.);
#2754=EDGE_CURVE('',#3417,#3416,#3899,.T.);
#2755=EDGE_CURVE('',#3418,#3417,#3900,.T.);
#2756=EDGE_CURVE('',#3419,#3418,#3901,.T.);
#2757=EDGE_CURVE('',#3420,#3419,#3902,.T.);
#2758=EDGE_CURVE('',#3421,#3420,#3903,.T.);
#2759=EDGE_CURVE('',#3422,#3421,#3904,.T.);
#2760=EDGE_CURVE('',#3423,#3422,#3905,.T.);
#2761=EDGE_CURVE('',#3424,#3423,#3906,.T.);
#2762=EDGE_CURVE('',#3425,#3424,#3907,.T.);
#2763=EDGE_CURVE('',#3426,#3425,#3908,.T.);
#2764=EDGE_CURVE('',#3427,#3426,#3909,.T.);
#2765=EDGE_CURVE('',#3428,#3427,#3910,.T.);
#2766=EDGE_CURVE('',#3429,#3428,#3911,.T.);
#2767=EDGE_CURVE('',#3430,#3429,#3912,.T.);
#2768=EDGE_CURVE('',#3431,#3430,#3913,.T.);
#2769=EDGE_CURVE('',#3432,#3431,#3914,.T.);
#2770=EDGE_CURVE('',#3433,#3432,#3915,.T.);
#2771=EDGE_CURVE('',#3434,#3433,#3916,.T.);
#2772=EDGE_CURVE('',#3435,#3434,#3917,.T.);
#2773=EDGE_CURVE('',#3436,#3435,#3918,.T.);
#2774=EDGE_CURVE('',#3437,#3436,#3919,.T.);
#2775=EDGE_CURVE('',#3438,#3437,#3920,.T.);
#2776=EDGE_CURVE('',#3439,#3438,#3921,.T.);
#2777=EDGE_CURVE('',#3440,#3439,#3922,.T.);
#2778=EDGE_CURVE('',#3441,#3440,#3923,.T.);
#2779=EDGE_CURVE('',#3442,#3441,#3924,.T.);
#2780=EDGE_CURVE('',#3443,#3442,#3925,.T.);
#2781=EDGE_CURVE('',#3444,#3443,#3926,.T.);
#2782=EDGE_CURVE('',#3445,#3444,#3927,.T.);
#2783=EDGE_CURVE('',#3446,#3445,#3928,.T.);
#2784=EDGE_CURVE('',#3447,#3446,#3929,.T.);
#2785=EDGE_CURVE('',#3448,#3447,#3930,.T.);
#2786=EDGE_CURVE('',#3449,#3448,#3931,.T.);
#2787=EDGE_CURVE('',#3450,#3449,#3932,.T.);
#2788=EDGE_CURVE('',#3451,#3450,#3933,.T.);
#2789=EDGE_CURVE('',#3452,#3451,#3934,.T.);
#2790=EDGE_CURVE('',#3453,#3452,#3935,.T.);
#2791=EDGE_CURVE('',#3454,#3453,#3936,.T.);
#2792=EDGE_CURVE('',#3455,#3454,#3937,.T.);
#2793=EDGE_CURVE('',#3456,#3455,#3938,.T.);
#2794=EDGE_CURVE('',#3457,#3456,#3939,.T.);
#2795=EDGE_CURVE('',#3458,#3457,#3940,.T.);
#2796=EDGE_CURVE('',#3459,#3458,#3941,.T.);
#2797=EDGE_CURVE('',#3460,#3459,#3942,.T.);
#2798=EDGE_CURVE('',#3374,#3460,#3943,.T.);
#2799=EDGE_CURVE('',#3374,#3461,#184,.T.);
#2800=EDGE_CURVE('',#3462,#3460,#185,.F.);
#2801=EDGE_CURVE('',#3461,#3462,#3944,.T.);
#2802=EDGE_CURVE('',#3463,#3376,#186,.F.);
#2803=EDGE_CURVE('',#3464,#3463,#3945,.T.);
#2804=EDGE_CURVE('',#3377,#3464,#187,.T.);
#2805=EDGE_CURVE('',#3457,#3465,#188,.T.);
#2806=EDGE_CURVE('',#3466,#3456,#189,.F.);
#2807=EDGE_CURVE('',#3465,#3466,#3946,.T.);
#2808=EDGE_CURVE('',#3453,#3467,#190,.T.);
#2809=EDGE_CURVE('',#3468,#3452,#191,.F.);
#2810=EDGE_CURVE('',#3467,#3468,#3947,.T.);
#2811=EDGE_CURVE('',#3445,#3469,#192,.T.);
#2812=EDGE_CURVE('',#3470,#3444,#193,.F.);
#2813=EDGE_CURVE('',#3469,#3470,#3948,.T.);
#2814=EDGE_CURVE('',#3471,#3448,#194,.F.);
#2815=EDGE_CURVE('',#3472,#3471,#3949,.T.);
#2816=EDGE_CURVE('',#3449,#3472,#195,.T.);
#2817=EDGE_CURVE('',#3393,#3473,#196,.T.);
#2818=EDGE_CURVE('',#3474,#3392,#197,.F.);
#2819=EDGE_CURVE('',#3473,#3474,#3950,.T.);
#2820=EDGE_CURVE('',#3475,#3396,#198,.F.);
#2821=EDGE_CURVE('',#3476,#3475,#3951,.T.);
#2822=EDGE_CURVE('',#3397,#3476,#199,.T.);
#2823=EDGE_CURVE('',#3389,#3477,#200,.T.);
#2824=EDGE_CURVE('',#3478,#3388,#201,.F.);
#2825=EDGE_CURVE('',#3477,#3478,#3952,.T.);
#2826=EDGE_CURVE('',#3385,#3479,#202,.T.);
#2827=EDGE_CURVE('',#3480,#3384,#203,.F.);
#2828=EDGE_CURVE('',#3479,#3480,#3953,.T.);
#2829=EDGE_CURVE('',#3481,#3380,#204,.F.);
#2830=EDGE_CURVE('',#3482,#3481,#3954,.T.);
#2831=EDGE_CURVE('',#3381,#3482,#205,.T.);
#2832=EDGE_CURVE('',#3405,#3483,#206,.T.);
#2833=EDGE_CURVE('',#3484,#3404,#207,.F.);
#2834=EDGE_CURVE('',#3483,#3484,#3955,.T.);
#2835=EDGE_CURVE('',#3485,#3408,#208,.F.);
#2836=EDGE_CURVE('',#3486,#3485,#3956,.T.);
#2837=EDGE_CURVE('',#3409,#3486,#209,.T.);
#2838=EDGE_CURVE('',#3487,#3412,#210,.F.);
#2839=EDGE_CURVE('',#3488,#3487,#3957,.T.);
#2840=EDGE_CURVE('',#3413,#3488,#211,.T.);
#2841=EDGE_CURVE('',#3489,#3416,#212,.F.);
#2842=EDGE_CURVE('',#3490,#3489,#3958,.T.);
#2843=EDGE_CURVE('',#3417,#3490,#213,.T.);
#2844=EDGE_CURVE('',#3401,#3491,#214,.T.);
#2845=EDGE_CURVE('',#3492,#3400,#215,.F.);
#2846=EDGE_CURVE('',#3491,#3492,#3959,.T.);
#2847=EDGE_CURVE('',#3425,#3493,#216,.T.);
#2848=EDGE_CURVE('',#3494,#3424,#217,.F.);
#2849=EDGE_CURVE('',#3493,#3494,#3960,.T.);
#2850=EDGE_CURVE('',#3495,#3428,#218,.F.);
#2851=EDGE_CURVE('',#3496,#3495,#3961,.T.);
#2852=EDGE_CURVE('',#3429,#3496,#219,.T.);
#2853=EDGE_CURVE('',#3497,#3432,#220,.F.);
#2854=EDGE_CURVE('',#3498,#3497,#3962,.T.);
#2855=EDGE_CURVE('',#3433,#3498,#221,.T.);
#2856=EDGE_CURVE('',#3499,#3436,#222,.F.);
#2857=EDGE_CURVE('',#3500,#3499,#3963,.T.);
#2858=EDGE_CURVE('',#3437,#3500,#223,.T.);
#2859=EDGE_CURVE('',#3421,#3501,#224,.T.);
#2860=EDGE_CURVE('',#3502,#3420,#225,.F.);
#2861=EDGE_CURVE('',#3501,#3502,#3964,.T.);
#2862=EDGE_CURVE('',#3503,#3461,#3965,.T.);
#2863=EDGE_CURVE('',#3504,#3462,#3966,.T.);
#2864=EDGE_CURVE('',#3504,#3505,#3967,.T.);
#2865=EDGE_CURVE('',#3505,#3465,#3968,.T.);
#2866=EDGE_CURVE('',#3506,#3466,#3969,.T.);
#2867=EDGE_CURVE('',#3506,#3507,#3970,.T.);
#2868=EDGE_CURVE('',#3507,#3467,#3971,.T.);
#2869=EDGE_CURVE('',#3508,#3468,#3972,.T.);
#2870=EDGE_CURVE('',#3508,#3509,#3973,.T.);
#2871=EDGE_CURVE('',#3509,#3472,#3974,.T.);
#2872=EDGE_CURVE('',#3510,#3471,#3975,.T.);
#2873=EDGE_CURVE('',#3510,#3511,#3976,.T.);
#2874=EDGE_CURVE('',#3511,#3469,#3977,.T.);
#2875=EDGE_CURVE('',#3512,#3470,#3978,.T.);
#2876=EDGE_CURVE('',#3512,#3513,#3979,.T.);
#2877=EDGE_CURVE('',#3513,#3514,#3980,.T.);
#2878=EDGE_CURVE('',#3514,#3515,#3981,.T.);
#2879=EDGE_CURVE('',#3516,#3515,#3982,.T.);
#2880=EDGE_CURVE('',#3516,#3517,#3983,.T.);
#2881=EDGE_CURVE('',#3517,#3500,#3984,.T.);
#2882=EDGE_CURVE('',#3518,#3499,#3985,.T.);
#2883=EDGE_CURVE('',#3518,#3519,#3986,.T.);
#2884=EDGE_CURVE('',#3519,#3498,#3987,.T.);
#2885=EDGE_CURVE('',#3520,#3497,#3988,.T.);
#2886=EDGE_CURVE('',#3520,#3521,#3989,.T.);
#2887=EDGE_CURVE('',#3521,#3496,#3990,.T.);
#2888=EDGE_CURVE('',#3522,#3495,#3991,.T.);
#2889=EDGE_CURVE('',#3522,#3523,#3992,.T.);
#2890=EDGE_CURVE('',#3523,#3493,#3993,.T.);
#2891=EDGE_CURVE('',#3524,#3494,#3994,.T.);
#2892=EDGE_CURVE('',#3524,#3525,#3995,.T.);
#2893=EDGE_CURVE('',#3525,#3501,#3996,.T.);
#2894=EDGE_CURVE('',#3526,#3502,#3997,.T.);
#2895=EDGE_CURVE('',#3526,#3527,#3998,.T.);
#2896=EDGE_CURVE('',#3527,#3490,#3999,.T.);
#2897=EDGE_CURVE('',#3528,#3489,#4000,.T.);
#2898=EDGE_CURVE('',#3528,#3529,#4001,.T.);
#2899=EDGE_CURVE('',#3529,#3488,#4002,.T.);
#2900=EDGE_CURVE('',#3530,#3487,#4003,.T.);
#2901=EDGE_CURVE('',#3530,#3531,#4004,.T.);
#2902=EDGE_CURVE('',#3531,#3486,#4005,.T.);
#2903=EDGE_CURVE('',#3532,#3485,#4006,.T.);
#2904=EDGE_CURVE('',#3532,#3533,#4007,.T.);
#2905=EDGE_CURVE('',#3533,#3483,#4008,.T.);
#2906=EDGE_CURVE('',#3534,#3484,#4009,.T.);
#2907=EDGE_CURVE('',#3534,#3535,#4010,.T.);
#2908=EDGE_CURVE('',#3535,#3491,#4011,.T.);
#2909=EDGE_CURVE('',#3536,#3492,#4012,.T.);
#2910=EDGE_CURVE('',#3536,#3537,#4013,.T.);
#2911=EDGE_CURVE('',#3537,#3476,#4014,.T.);
#2912=EDGE_CURVE('',#3538,#3475,#4015,.T.);
#2913=EDGE_CURVE('',#3538,#3539,#4016,.T.);
#2914=EDGE_CURVE('',#3539,#3473,#4017,.T.);
#2915=EDGE_CURVE('',#3540,#3474,#4018,.T.);
#2916=EDGE_CURVE('',#3540,#3541,#4019,.T.);
#2917=EDGE_CURVE('',#3541,#3477,#4020,.T.);
#2918=EDGE_CURVE('',#3542,#3478,#4021,.T.);
#2919=EDGE_CURVE('',#3542,#3543,#4022,.T.);
#2920=EDGE_CURVE('',#3543,#3479,#4023,.T.);
#2921=EDGE_CURVE('',#3544,#3480,#4024,.T.);
#2922=EDGE_CURVE('',#3544,#3545,#4025,.T.);
#2923=EDGE_CURVE('',#3545,#3482,#4026,.T.);
#2924=EDGE_CURVE('',#3546,#3481,#4027,.T.);
#2925=EDGE_CURVE('',#3546,#3547,#4028,.T.);
#2926=EDGE_CURVE('',#3547,#3464,#4029,.T.);
#2927=EDGE_CURVE('',#3548,#3463,#4030,.T.);
#2928=EDGE_CURVE('',#3548,#3503,#4031,.T.);
#2929=EDGE_CURVE('',#3441,#3514,#226,.T.);
#2930=EDGE_CURVE('',#3515,#3440,#227,.F.);
#2931=EDGE_CURVE('',#3438,#3517,#228,.T.);
#2932=EDGE_CURVE('',#3439,#3516,#229,.T.);
#2933=EDGE_CURVE('',#3442,#3513,#230,.T.);
#2934=EDGE_CURVE('',#3443,#3512,#231,.T.);
#2935=EDGE_CURVE('',#3418,#3527,#232,.T.);
#2936=EDGE_CURVE('',#3419,#3526,#233,.T.);
#2937=EDGE_CURVE('',#3422,#3525,#234,.T.);
#2938=EDGE_CURVE('',#3423,#3524,#235,.T.);
#2939=EDGE_CURVE('',#3434,#3519,#236,.T.);
#2940=EDGE_CURVE('',#3435,#3518,#237,.T.);
#2941=EDGE_CURVE('',#3430,#3521,#238,.T.);
#2942=EDGE_CURVE('',#3431,#3520,#239,.T.);
#2943=EDGE_CURVE('',#3426,#3523,#240,.T.);
#2944=EDGE_CURVE('',#3427,#3522,#241,.T.);
#2945=EDGE_CURVE('',#3398,#3537,#242,.T.);
#2946=EDGE_CURVE('',#3399,#3536,#243,.T.);
#2947=EDGE_CURVE('',#3402,#3535,#244,.T.);
#2948=EDGE_CURVE('',#3403,#3534,#245,.T.);
#2949=EDGE_CURVE('',#3414,#3529,#246,.T.);
#2950=EDGE_CURVE('',#3415,#3528,#247,.T.);
#2951=EDGE_CURVE('',#3410,#3531,#248,.T.);
#2952=EDGE_CURVE('',#3411,#3530,#249,.T.);
#2953=EDGE_CURVE('',#3406,#3533,#250,.T.);
#2954=EDGE_CURVE('',#3407,#3532,#251,.T.);
#2955=EDGE_CURVE('',#3382,#3545,#252,.T.);
#2956=EDGE_CURVE('',#3383,#3544,#253,.T.);
#2957=EDGE_CURVE('',#3378,#3547,#254,.T.);
#2958=EDGE_CURVE('',#3379,#3546,#255,.T.);
#2959=EDGE_CURVE('',#3386,#3543,#256,.T.);
#2960=EDGE_CURVE('',#3387,#3542,#257,.T.);
#2961=EDGE_CURVE('',#3390,#3541,#258,.T.);
#2962=EDGE_CURVE('',#3391,#3540,#259,.T.);
#2963=EDGE_CURVE('',#3394,#3539,#260,.T.);
#2964=EDGE_CURVE('',#3395,#3538,#261,.T.);
#2965=EDGE_CURVE('',#3450,#3509,#262,.T.);
#2966=EDGE_CURVE('',#3451,#3508,#263,.T.);
#2967=EDGE_CURVE('',#3446,#3511,#264,.T.);
#2968=EDGE_CURVE('',#3447,#3510,#265,.T.);
#2969=EDGE_CURVE('',#3454,#3507,#266,.T.);
#2970=EDGE_CURVE('',#3455,#3506,#267,.T.);
#2971=EDGE_CURVE('',#3458,#3505,#268,.T.);
#2972=EDGE_CURVE('',#3459,#3504,#269,.T.);
#2973=EDGE_CURVE('',#3373,#3503,#270,.T.);
#2974=EDGE_CURVE('',#3375,#3548,#271,.T.);
#2975=EDGE_CURVE('',#3549,#3549,#4032,.T.);
#2976=EDGE_CURVE('',#3550,#3550,#4033,.T.);
#2977=EDGE_CURVE('',#3551,#3551,#4034,.T.);
#2978=EDGE_CURVE('',#3552,#3552,#4035,.T.);
#2979=EDGE_CURVE('',#3553,#3553,#4036,.T.);
#2980=EDGE_CURVE('',#3554,#3554,#4037,.T.);
#3369=VERTEX_POINT('',#9236);
#3370=VERTEX_POINT('',#9238);
#3371=VERTEX_POINT('',#9241);
#3372=VERTEX_POINT('',#9243);
#3373=VERTEX_POINT('',#9246);
#3374=VERTEX_POINT('',#9247);
#3375=VERTEX_POINT('',#9249);
#3376=VERTEX_POINT('',#9251);
#3377=VERTEX_POINT('',#9253);
#3378=VERTEX_POINT('',#9255);
#3379=VERTEX_POINT('',#9257);
#3380=VERTEX_POINT('',#9259);
#3381=VERTEX_POINT('',#9261);
#3382=VERTEX_POINT('',#9263);
#3383=VERTEX_POINT('',#9265);
#3384=VERTEX_POINT('',#9267);
#3385=VERTEX_POINT('',#9269);
#3386=VERTEX_POINT('',#9271);
#3387=VERTEX_POINT('',#9273);
#3388=VERTEX_POINT('',#9275);
#3389=VERTEX_POINT('',#9277);
#3390=VERTEX_POINT('',#9279);
#3391=VERTEX_POINT('',#9281);
#3392=VERTEX_POINT('',#9283);
#3393=VERTEX_POINT('',#9285);
#3394=VERTEX_POINT('',#9287);
#3395=VERTEX_POINT('',#9289);
#3396=VERTEX_POINT('',#9291);
#3397=VERTEX_POINT('',#9293);
#3398=VERTEX_POINT('',#9295);
#3399=VERTEX_POINT('',#9297);
#3400=VERTEX_POINT('',#9299);
#3401=VERTEX_POINT('',#9301);
#3402=VERTEX_POINT('',#9303);
#3403=VERTEX_POINT('',#9305);
#3404=VERTEX_POINT('',#9307);
#3405=VERTEX_POINT('',#9309);
#3406=VERTEX_POINT('',#9311);
#3407=VERTEX_POINT('',#9313);
#3408=VERTEX_POINT('',#9315);
#3409=VERTEX_POINT('',#9317);
#3410=VERTEX_POINT('',#9319);
#3411=VERTEX_POINT('',#9321);
#3412=VERTEX_POINT('',#9323);
#3413=VERTEX_POINT('',#9325);
#3414=VERTEX_POINT('',#9327);
#3415=VERTEX_POINT('',#9329);
#3416=VERTEX_POINT('',#9331);
#3417=VERTEX_POINT('',#9333);
#3418=VERTEX_POINT('',#9335);
#3419=VERTEX_POINT('',#9337);
#3420=VERTEX_POINT('',#9339);
#3421=VERTEX_POINT('',#9341);
#3422=VERTEX_POINT('',#9343);
#3423=VERTEX_POINT('',#9345);
#3424=VERTEX_POINT('',#9347);
#3425=VERTEX_POINT('',#9349);
#3426=VERTEX_POINT('',#9351);
#3427=VERTEX_POINT('',#9353);
#3428=VERTEX_POINT('',#9355);
#3429=VERTEX_POINT('',#9357);
#3430=VERTEX_POINT('',#9359);
#3431=VERTEX_POINT('',#9361);
#3432=VERTEX_POINT('',#9363);
#3433=VERTEX_POINT('',#9365);
#3434=VERTEX_POINT('',#9367);
#3435=VERTEX_POINT('',#9369);
#3436=VERTEX_POINT('',#9371);
#3437=VERTEX_POINT('',#9373);
#3438=VERTEX_POINT('',#9375);
#3439=VERTEX_POINT('',#9377);
#3440=VERTEX_POINT('',#9379);
#3441=VERTEX_POINT('',#9381);
#3442=VERTEX_POINT('',#9383);
#3443=VERTEX_POINT('',#9385);
#3444=VERTEX_POINT('',#9387);
#3445=VERTEX_POINT('',#9389);
#3446=VERTEX_POINT('',#9391);
#3447=VERTEX_POINT('',#9393);
#3448=VERTEX_POINT('',#9395);
#3449=VERTEX_POINT('',#9397);
#3450=VERTEX_POINT('',#9399);
#3451=VERTEX_POINT('',#9401);
#3452=VERTEX_POINT('',#9403);
#3453=VERTEX_POINT('',#9405);
#3454=VERTEX_POINT('',#9407);
#3455=VERTEX_POINT('',#9409);
#3456=VERTEX_POINT('',#9411);
#3457=VERTEX_POINT('',#9413);
#3458=VERTEX_POINT('',#9415);
#3459=VERTEX_POINT('',#9417);
#3460=VERTEX_POINT('',#9419);
#3461=VERTEX_POINT('',#9423);
#3462=VERTEX_POINT('',#9425);
#3463=VERTEX_POINT('',#9429);
#3464=VERTEX_POINT('',#9431);
#3465=VERTEX_POINT('',#9435);
#3466=VERTEX_POINT('',#9437);
#3467=VERTEX_POINT('',#9441);
#3468=VERTEX_POINT('',#9443);
#3469=VERTEX_POINT('',#9447);
#3470=VERTEX_POINT('',#9449);
#3471=VERTEX_POINT('',#9453);
#3472=VERTEX_POINT('',#9455);
#3473=VERTEX_POINT('',#9459);
#3474=VERTEX_POINT('',#9461);
#3475=VERTEX_POINT('',#9465);
#3476=VERTEX_POINT('',#9467);
#3477=VERTEX_POINT('',#9471);
#3478=VERTEX_POINT('',#9473);
#3479=VERTEX_POINT('',#9477);
#3480=VERTEX_POINT('',#9479);
#3481=VERTEX_POINT('',#9483);
#3482=VERTEX_POINT('',#9485);
#3483=VERTEX_POINT('',#9489);
#3484=VERTEX_POINT('',#9491);
#3485=VERTEX_POINT('',#9495);
#3486=VERTEX_POINT('',#9497);
#3487=VERTEX_POINT('',#9501);
#3488=VERTEX_POINT('',#9503);
#3489=VERTEX_POINT('',#9507);
#3490=VERTEX_POINT('',#9509);
#3491=VERTEX_POINT('',#9513);
#3492=VERTEX_POINT('',#9515);
#3493=VERTEX_POINT('',#9519);
#3494=VERTEX_POINT('',#9521);
#3495=VERTEX_POINT('',#9525);
#3496=VERTEX_POINT('',#9527);
#3497=VERTEX_POINT('',#9531);
#3498=VERTEX_POINT('',#9533);
#3499=VERTEX_POINT('',#9537);
#3500=VERTEX_POINT('',#9539);
#3501=VERTEX_POINT('',#9543);
#3502=VERTEX_POINT('',#9545);
#3503=VERTEX_POINT('',#9549);
#3504=VERTEX_POINT('',#9551);
#3505=VERTEX_POINT('',#9553);
#3506=VERTEX_POINT('',#9556);
#3507=VERTEX_POINT('',#9558);
#3508=VERTEX_POINT('',#9561);
#3509=VERTEX_POINT('',#9563);
#3510=VERTEX_POINT('',#9566);
#3511=VERTEX_POINT('',#9568);
#3512=VERTEX_POINT('',#9571);
#3513=VERTEX_POINT('',#9573);
#3514=VERTEX_POINT('',#9575);
#3515=VERTEX_POINT('',#9577);
#3516=VERTEX_POINT('',#9579);
#3517=VERTEX_POINT('',#9581);
#3518=VERTEX_POINT('',#9584);
#3519=VERTEX_POINT('',#9586);
#3520=VERTEX_POINT('',#9589);
#3521=VERTEX_POINT('',#9591);
#3522=VERTEX_POINT('',#9594);
#3523=VERTEX_POINT('',#9596);
#3524=VERTEX_POINT('',#9599);
#3525=VERTEX_POINT('',#9601);
#3526=VERTEX_POINT('',#9604);
#3527=VERTEX_POINT('',#9606);
#3528=VERTEX_POINT('',#9609);
#3529=VERTEX_POINT('',#9611);
#3530=VERTEX_POINT('',#9614);
#3531=VERTEX_POINT('',#9616);
#3532=VERTEX_POINT('',#9619);
#3533=VERTEX_POINT('',#9621);
#3534=VERTEX_POINT('',#9624);
#3535=VERTEX_POINT('',#9626);
#3536=VERTEX_POINT('',#9629);
#3537=VERTEX_POINT('',#9631);
#3538=VERTEX_POINT('',#9634);
#3539=VERTEX_POINT('',#9636);
#3540=VERTEX_POINT('',#9639);
#3541=VERTEX_POINT('',#9641);
#3542=VERTEX_POINT('',#9644);
#3543=VERTEX_POINT('',#9646);
#3544=VERTEX_POINT('',#9649);
#3545=VERTEX_POINT('',#9651);
#3546=VERTEX_POINT('',#9654);
#3547=VERTEX_POINT('',#9656);
#3548=VERTEX_POINT('',#9659);
#3549=VERTEX_POINT('',#9776);
#3550=VERTEX_POINT('',#9778);
#3551=VERTEX_POINT('',#9781);
#3552=VERTEX_POINT('',#9786);
#3553=VERTEX_POINT('',#9788);
#3554=VERTEX_POINT('',#9791);
#3852=CIRCLE('',#6075,0.0015);
#3853=CIRCLE('',#6076,0.0015);
#3854=CIRCLE('',#6078,0.0025);
#3855=CIRCLE('',#6079,0.0025);
#3856=CIRCLE('',#6081,0.0022);
#3857=CIRCLE('',#6082,0.004874);
#3858=CIRCLE('',#6083,0.0022);
#3859=CIRCLE('',#6084,0.006);
#3860=CIRCLE('',#6085,0.0022);
#3861=CIRCLE('',#6086,0.004874);
#3862=CIRCLE('',#6087,0.0022);
#3863=CIRCLE('',#6088,0.006);
#3864=CIRCLE('',#6089,0.0022);
#3865=CIRCLE('',#6090,0.004874);
#3866=CIRCLE('',#6091,0.0022);
#3867=CIRCLE('',#6092,0.006);
#3868=CIRCLE('',#6093,0.0022);
#3869=CIRCLE('',#6094,0.004874);
#3870=CIRCLE('',#6095,0.0022);
#3871=CIRCLE('',#6096,0.006);
#3872=CIRCLE('',#6097,0.0022);
#3873=CIRCLE('',#6098,0.004874);
#3874=CIRCLE('',#6099,0.0022);
#3875=CIRCLE('',#6100,0.006);
#3876=CIRCLE('',#6101,0.0022);
#3877=CIRCLE('',#6102,0.004874);
#3878=CIRCLE('',#6103,0.0022);
#3879=CIRCLE('',#6104,0.006);
#3880=CIRCLE('',#6105,0.0022);
#3881=CIRCLE('',#6106,0.004874);
#3882=CIRCLE('',#6107,0.0022);
#3883=CIRCLE('',#6108,0.006);
#3884=CIRCLE('',#6109,0.0022);
#3885=CIRCLE('',#6110,0.004874);
#3886=CIRCLE('',#6111,0.0022);
#3887=CIRCLE('',#6112,0.006);
#3888=CIRCLE('',#6113,0.0022);
#3889=CIRCLE('',#6114,0.004874);
#3890=CIRCLE('',#6115,0.0022);
#3891=CIRCLE('',#6116,0.006);
#3892=CIRCLE('',#6117,0.0022);
#3893=CIRCLE('',#6118,0.004874);
#3894=CIRCLE('',#6119,0.0022);
#3895=CIRCLE('',#6120,0.006);
#3896=CIRCLE('',#6121,0.0022);
#3897=CIRCLE('',#6122,0.004874);
#3898=CIRCLE('',#6123,0.0022);
#3899=CIRCLE('',#6124,0.006);
#3900=CIRCLE('',#6125,0.0022);
#3901=CIRCLE('',#6126,0.004874);
#3902=CIRCLE('',#6127,0.0022);
#3903=CIRCLE('',#6128,0.006);
#3904=CIRCLE('',#6129,0.0022);
#3905=CIRCLE('',#6130,0.004874);
#3906=CIRCLE('',#6131,0.0022);
#3907=CIRCLE('',#6132,0.006);
#3908=CIRCLE('',#6133,0.0022);
#3909=CIRCLE('',#6134,0.004874);
#3910=CIRCLE('',#6135,0.0022);
#3911=CIRCLE('',#6136,0.006);
#3912=CIRCLE('',#6137,0.0022);
#3913=CIRCLE('',#6138,0.004874);
#3914=CIRCLE('',#6139,0.0022);
#3915=CIRCLE('',#6140,0.006);
#3916=CIRCLE('',#6141,0.0022);
#3917=CIRCLE('',#6142,0.004874);
#3918=CIRCLE('',#6143,0.0022);
#3919=CIRCLE('',#6144,0.006);
#3920=CIRCLE('',#6145,0.0022);
#3921=CIRCLE('',#6146,0.004874);
#3922=CIRCLE('',#6147,0.0022);
#3923=CIRCLE('',#6148,0.006);
#3924=CIRCLE('',#6149,0.0022);
#3925=CIRCLE('',#6150,0.004874);
#3926=CIRCLE('',#6151,0.0022);
#3927=CIRCLE('',#6152,0.006);
#3928=CIRCLE('',#6153,0.0022);
#3929=CIRCLE('',#6154,0.004874);
#3930=CIRCLE('',#6155,0.0022);
#3931=CIRCLE('',#6156,0.006);
#3932=CIRCLE('',#6157,0.0022);
#3933=CIRCLE('',#6158,0.004874);
#3934=CIRCLE('',#6159,0.0022);
#3935=CIRCLE('',#6160,0.006);
#3936=CIRCLE('',#6161,0.0022);
#3937=CIRCLE('',#6162,0.004874);
#3938=CIRCLE('',#6163,0.0022);
#3939=CIRCLE('',#6164,0.006);
#3940=CIRCLE('',#6165,0.0022);
#3941=CIRCLE('',#6166,0.004874);
#3942=CIRCLE('',#6167,0.0022);
#3943=CIRCLE('',#6168,0.006);
#3944=CIRCLE('',#6170,0.006);
#3945=CIRCLE('',#6172,0.006);
#3946=CIRCLE('',#6174,0.006);
#3947=CIRCLE('',#6176,0.006);
#3948=CIRCLE('',#6178,0.006);
#3949=CIRCLE('',#6180,0.006);
#3950=CIRCLE('',#6182,0.006);
#3951=CIRCLE('',#6184,0.006);
#3952=CIRCLE('',#6186,0.006);
#3953=CIRCLE('',#6188,0.006);
#3954=CIRCLE('',#6190,0.006);
#3955=CIRCLE('',#6192,0.006);
#3956=CIRCLE('',#6194,0.006);
#3957=CIRCLE('',#6196,0.006);
#3958=CIRCLE('',#6198,0.006);
#3959=CIRCLE('',#6200,0.006);
#3960=CIRCLE('',#6202,0.006);
#3961=CIRCLE('',#6204,0.006);
#3962=CIRCLE('',#6206,0.006);
#3963=CIRCLE('',#6208,0.006);
#3964=CIRCLE('',#6210,0.006);
#3965=CIRCLE('',#6212,0.0022);
#3966=CIRCLE('',#6213,0.0022);
#3967=CIRCLE('',#6214,0.004874);
#3968=CIRCLE('',#6215,0.0022);
#3969=CIRCLE('',#6216,0.0022);
#3970=CIRCLE('',#6217,0.004874);
#3971=CIRCLE('',#6218,0.0022);
#3972=CIRCLE('',#6219,0.0022);
#3973=CIRCLE('',#6220,0.004874);
#3974=CIRCLE('',#6221,0.0022);
#3975=CIRCLE('',#6222,0.0022);
#3976=CIRCLE('',#6223,0.004874);
#3977=CIRCLE('',#6224,0.0022);
#3978=CIRCLE('',#6225,0.0022);
#3979=CIRCLE('',#6226,0.004874);
#3980=CIRCLE('',#6227,0.0022);
#3981=CIRCLE('',#6228,0.006);
#3982=CIRCLE('',#6229,0.0022);
#3983=CIRCLE('',#6230,0.004874);
#3984=CIRCLE('',#6231,0.0022);
#3985=CIRCLE('',#6232,0.0022);
#3986=CIRCLE('',#6233,0.004874);
#3987=CIRCLE('',#6234,0.0022);
#3988=CIRCLE('',#6235,0.0022);
#3989=CIRCLE('',#6236,0.004874);
#3990=CIRCLE('',#6237,0.0022);
#3991=CIRCLE('',#6238,0.0022);
#3992=CIRCLE('',#6239,0.004874);
#3993=CIRCLE('',#6240,0.0022);
#3994=CIRCLE('',#6241,0.0022);
#3995=CIRCLE('',#6242,0.004874);
#3996=CIRCLE('',#6243,0.0022);
#3997=CIRCLE('',#6244,0.0022);
#3998=CIRCLE('',#6245,0.004874);
#3999=CIRCLE('',#6246,0.0022);
#4000=CIRCLE('',#6247,0.0022);
#4001=CIRCLE('',#6248,0.004874);
#4002=CIRCLE('',#6249,0.0022);
#4003=CIRCLE('',#6250,0.0022);
#4004=CIRCLE('',#6251,0.004874);
#4005=CIRCLE('',#6252,0.0022);
#4006=CIRCLE('',#6253,0.0022);
#4007=CIRCLE('',#6254,0.004874);
#4008=CIRCLE('',#6255,0.0022);
#4009=CIRCLE('',#6256,0.0022);
#4010=CIRCLE('',#6257,0.004874);
#4011=CIRCLE('',#6258,0.0022);
#4012=CIRCLE('',#6259,0.0022);
#4013=CIRCLE('',#6260,0.004874);
#4014=CIRCLE('',#6261,0.0022);
#4015=CIRCLE('',#6262,0.0022);
#4016=CIRCLE('',#6263,0.004874);
#4017=CIRCLE('',#6264,0.0022);
#4018=CIRCLE('',#6265,0.0022);
#4019=CIRCLE('',#6266,0.004874);
#4020=CIRCLE('',#6267,0.0022);
#4021=CIRCLE('',#6268,0.0022);
#4022=CIRCLE('',#6269,0.004874);
#4023=CIRCLE('',#6270,0.0022);
#4024=CIRCLE('',#6271,0.0022);
#4025=CIRCLE('',#6272,0.004874);
#4026=CIRCLE('',#6273,0.0022);
#4027=CIRCLE('',#6274,0.0022);
#4028=CIRCLE('',#6275,0.004874);
#4029=CIRCLE('',#6276,0.0022);
#4030=CIRCLE('',#6277,0.0022);
#4031=CIRCLE('',#6278,0.004874);
#4032=CIRCLE('',#6347,0.0025);
#4033=CIRCLE('',#6348,0.00375738138352587);
#4034=CIRCLE('',#6350,0.00375738138352587);
#4035=CIRCLE('',#6354,0.0015);
#4036=CIRCLE('',#6355,0.0015);
#4037=CIRCLE('',#6357,0.0025);
#4342=EDGE_LOOP('',(#1540));
#4343=EDGE_LOOP('',(#1541));
#4344=EDGE_LOOP('',(#1542));
#4345=EDGE_LOOP('',(#1543));
#4346=EDGE_LOOP('',(#1544,#1545,#1546,#1547,#1548,#1549,#1550,#1551,#1552,
#1553,#1554,#1555,#1556,#1557,#1558,#1559,#1560,#1561,#1562,#1563,#1564,
#1565,#1566,#1567,#1568,#1569,#1570,#1571,#1572,#1573,#1574,#1575,#1576,
#1577,#1578,#1579,#1580,#1581,#1582,#1583,#1584,#1585,#1586,#1587,#1588,
#1589,#1590,#1591,#1592,#1593,#1594,#1595,#1596,#1597,#1598,#1599,#1600,
#1601,#1602,#1603,#1604,#1605,#1606,#1607,#1608,#1609,#1610,#1611,#1612,
#1613,#1614,#1615,#1616,#1617,#1618,#1619,#1620,#1621,#1622,#1623,#1624,
#1625,#1626,#1627,#1628,#1629,#1630,#1631));
#4347=EDGE_LOOP('',(#1632));
#4348=EDGE_LOOP('',(#1633,#1634,#1635,#1636));
#4349=EDGE_LOOP('',(#1637,#1638,#1639,#1640));
#4350=EDGE_LOOP('',(#1641,#1642,#1643,#1644));
#4351=EDGE_LOOP('',(#1645,#1646,#1647,#1648));
#4352=EDGE_LOOP('',(#1649,#1650,#1651,#1652));
#4353=EDGE_LOOP('',(#1653,#1654,#1655,#1656));
#4354=EDGE_LOOP('',(#1657,#1658,#1659,#1660));
#4355=EDGE_LOOP('',(#1661,#1662,#1663,#1664));
#4356=EDGE_LOOP('',(#1665,#1666,#1667,#1668));
#4357=EDGE_LOOP('',(#1669,#1670,#1671,#1672));
#4358=EDGE_LOOP('',(#1673,#1674,#1675,#1676));
#4359=EDGE_LOOP('',(#1677,#1678,#1679,#1680));
#4360=EDGE_LOOP('',(#1681,#1682,#1683,#1684));
#4361=EDGE_LOOP('',(#1685,#1686,#1687,#1688));
#4362=EDGE_LOOP('',(#1689,#1690,#1691,#1692));
#4363=EDGE_LOOP('',(#1693,#1694,#1695,#1696));
#4364=EDGE_LOOP('',(#1697,#1698,#1699,#1700));
#4365=EDGE_LOOP('',(#1701,#1702,#1703,#1704));
#4366=EDGE_LOOP('',(#1705,#1706,#1707,#1708));
#4367=EDGE_LOOP('',(#1709,#1710,#1711,#1712));
#4368=EDGE_LOOP('',(#1713,#1714,#1715,#1716));
#4369=EDGE_LOOP('',(#1717));
#4370=EDGE_LOOP('',(#1718,#1719,#1720,#1721,#1722,#1723,#1724,#1725,#1726,
#1727,#1728,#1729,#1730,#1731,#1732,#1733,#1734,#1735,#1736,#1737,#1738,
#1739,#1740,#1741,#1742,#1743,#1744,#1745,#1746,#1747,#1748,#1749,#1750,
#1751,#1752,#1753,#1754,#1755,#1756,#1757,#1758,#1759,#1760,#1761,#1762,
#1763,#1764,#1765,#1766,#1767,#1768,#1769,#1770,#1771,#1772,#1773,#1774,
#1775,#1776,#1777,#1778,#1779,#1780,#1781,#1782,#1783,#1784,#1785,#1786,
#1787,#1788,#1789,#1790,#1791,#1792,#1793,#1794,#1795,#1796,#1797,#1798,
#1799,#1800,#1801,#1802,#1803,#1804,#1805));
#4371=EDGE_LOOP('',(#1806,#1807,#1808,#1809));
#4372=EDGE_LOOP('',(#1810,#1811,#1812,#1813));
#4373=EDGE_LOOP('',(#1814,#1815,#1816,#1817));
#4374=EDGE_LOOP('',(#1818,#1819,#1820,#1821));
#4375=EDGE_LOOP('',(#1822,#1823,#1824,#1825));
#4376=EDGE_LOOP('',(#1826,#1827,#1828,#1829));
#4377=EDGE_LOOP('',(#1830,#1831,#1832,#1833));
#4378=EDGE_LOOP('',(#1834,#1835,#1836,#1837));
#4379=EDGE_LOOP('',(#1838,#1839,#1840,#1841));
#4380=EDGE_LOOP('',(#1842,#1843,#1844,#1845));
#4381=EDGE_LOOP('',(#1846,#1847,#1848,#1849));
#4382=EDGE_LOOP('',(#1850,#1851,#1852,#1853));
#4383=EDGE_LOOP('',(#1854,#1855,#1856,#1857));
#4384=EDGE_LOOP('',(#1858,#1859,#1860,#1861));
#4385=EDGE_LOOP('',(#1862,#1863,#1864,#1865));
#4386=EDGE_LOOP('',(#1866,#1867,#1868,#1869));
#4387=EDGE_LOOP('',(#1870,#1871,#1872,#1873));
#4388=EDGE_LOOP('',(#1874,#1875,#1876,#1877));
#4389=EDGE_LOOP('',(#1878,#1879,#1880,#1881));
#4390=EDGE_LOOP('',(#1882,#1883,#1884,#1885));
#4391=EDGE_LOOP('',(#1886,#1887,#1888,#1889));
#4392=EDGE_LOOP('',(#1890,#1891,#1892,#1893));
#4393=EDGE_LOOP('',(#1894,#1895,#1896,#1897));
#4394=EDGE_LOOP('',(#1898,#1899,#1900,#1901));
#4395=EDGE_LOOP('',(#1902,#1903,#1904,#1905));
#4396=EDGE_LOOP('',(#1906,#1907,#1908,#1909));
#4397=EDGE_LOOP('',(#1910,#1911,#1912,#1913));
#4398=EDGE_LOOP('',(#1914,#1915,#1916,#1917));
#4399=EDGE_LOOP('',(#1918,#1919,#1920,#1921));
#4400=EDGE_LOOP('',(#1922,#1923,#1924,#1925));
#4401=EDGE_LOOP('',(#1926,#1927,#1928,#1929));
#4402=EDGE_LOOP('',(#1930,#1931,#1932,#1933));
#4403=EDGE_LOOP('',(#1934,#1935,#1936,#1937));
#4404=EDGE_LOOP('',(#1938,#1939,#1940,#1941));
#4405=EDGE_LOOP('',(#1942,#1943,#1944,#1945));
#4406=EDGE_LOOP('',(#1946,#1947,#1948,#1949));
#4407=EDGE_LOOP('',(#1950,#1951,#1952,#1953));
#4408=EDGE_LOOP('',(#1954,#1955,#1956,#1957));
#4409=EDGE_LOOP('',(#1958,#1959,#1960,#1961));
#4410=EDGE_LOOP('',(#1962,#1963,#1964,#1965));
#4411=EDGE_LOOP('',(#1966,#1967,#1968,#1969));
#4412=EDGE_LOOP('',(#1970,#1971,#1972,#1973));
#4413=EDGE_LOOP('',(#1974,#1975,#1976,#1977));
#4414=EDGE_LOOP('',(#1978,#1979,#1980,#1981));
#4415=EDGE_LOOP('',(#1982,#1983,#1984,#1985));
#4416=EDGE_LOOP('',(#1986,#1987,#1988,#1989));
#4417=EDGE_LOOP('',(#1990,#1991,#1992,#1993));
#4418=EDGE_LOOP('',(#1994,#1995,#1996,#1997));
#4419=EDGE_LOOP('',(#1998,#1999,#2000,#2001));
#4420=EDGE_LOOP('',(#2002,#2003,#2004,#2005));
#4421=EDGE_LOOP('',(#2006,#2007,#2008,#2009));
#4422=EDGE_LOOP('',(#2010,#2011,#2012,#2013));
#4423=EDGE_LOOP('',(#2014,#2015,#2016,#2017));
#4424=EDGE_LOOP('',(#2018,#2019,#2020,#2021));
#4425=EDGE_LOOP('',(#2022,#2023,#2024,#2025));
#4426=EDGE_LOOP('',(#2026,#2027,#2028,#2029));
#4427=EDGE_LOOP('',(#2030,#2031,#2032,#2033));
#4428=EDGE_LOOP('',(#2034,#2035,#2036,#2037));
#4429=EDGE_LOOP('',(#2038,#2039,#2040,#2041));
#4430=EDGE_LOOP('',(#2042,#2043,#2044,#2045));
#4431=EDGE_LOOP('',(#2046,#2047,#2048,#2049));
#4432=EDGE_LOOP('',(#2050,#2051,#2052,#2053));
#4433=EDGE_LOOP('',(#2054,#2055,#2056,#2057));
#4434=EDGE_LOOP('',(#2058,#2059,#2060,#2061));
#4435=EDGE_LOOP('',(#2062,#2063,#2064,#2065));
#4436=EDGE_LOOP('',(#2066,#2067,#2068,#2069));
#4437=EDGE_LOOP('',(#2070,#2071,#2072,#2073));
#4438=EDGE_LOOP('',(#2074));
#4439=EDGE_LOOP('',(#2075));
#4440=EDGE_LOOP('',(#2076));
#4441=EDGE_LOOP('',(#2077));
#4442=EDGE_LOOP('',(#2078));
#4443=EDGE_LOOP('',(#2079));
#4444=EDGE_LOOP('',(#2080));
#4445=EDGE_LOOP('',(#2081));
#4446=EDGE_LOOP('',(#2082));
#4447=EDGE_LOOP('',(#2083));
#4448=EDGE_LOOP('',(#2084));
#4449=EDGE_LOOP('',(#2085));
#4450=EDGE_LOOP('',(#2086));
#4451=EDGE_LOOP('',(#2087));
#4790=FACE_BOUND('',#4342,.T.);
#4791=FACE_BOUND('',#4343,.T.);
#4792=FACE_BOUND('',#4344,.T.);
#4793=FACE_BOUND('',#4345,.T.);
#4794=FACE_BOUND('',#4346,.T.);
#4795=FACE_BOUND('',#4347,.T.);
#4796=FACE_BOUND('',#4348,.T.);
#4797=FACE_BOUND('',#4349,.T.);
#4798=FACE_BOUND('',#4350,.T.);
#4799=FACE_BOUND('',#4351,.T.);
#4800=FACE_BOUND('',#4352,.T.);
#4801=FACE_BOUND('',#4353,.T.);
#4802=FACE_BOUND('',#4354,.T.);
#4803=FACE_BOUND('',#4355,.T.);
#4804=FACE_BOUND('',#4356,.T.);
#4805=FACE_BOUND('',#4357,.T.);
#4806=FACE_BOUND('',#4358,.T.);
#4807=FACE_BOUND('',#4359,.T.);
#4808=FACE_BOUND('',#4360,.T.);
#4809=FACE_BOUND('',#4361,.T.);
#4810=FACE_BOUND('',#4362,.T.);
#4811=FACE_BOUND('',#4363,.T.);
#4812=FACE_BOUND('',#4364,.T.);
#4813=FACE_BOUND('',#4365,.T.);
#4814=FACE_BOUND('',#4366,.T.);
#4815=FACE_BOUND('',#4367,.T.);
#4816=FACE_BOUND('',#4368,.T.);
#4817=FACE_BOUND('',#4369,.T.);
#4818=FACE_BOUND('',#4370,.T.);
#4819=FACE_BOUND('',#4371,.T.);
#4820=FACE_BOUND('',#4372,.T.);
#4821=FACE_BOUND('',#4373,.T.);
#4822=FACE_BOUND('',#4374,.T.);
#4823=FACE_BOUND('',#4375,.T.);
#4824=FACE_BOUND('',#4376,.T.);
#4825=FACE_BOUND('',#4377,.T.);
#4826=FACE_BOUND('',#4378,.T.);
#4827=FACE_BOUND('',#4379,.T.);
#4828=FACE_BOUND('',#4380,.T.);
#4829=FACE_BOUND('',#4381,.T.);
#4830=FACE_BOUND('',#4382,.T.);
#4831=FACE_BOUND('',#4383,.T.);
#4832=FACE_BOUND('',#4384,.T.);
#4833=FACE_BOUND('',#4385,.T.);
#4834=FACE_BOUND('',#4386,.T.);
#4835=FACE_BOUND('',#4387,.T.);
#4836=FACE_BOUND('',#4388,.T.);
#4837=FACE_BOUND('',#4389,.T.);
#4838=FACE_BOUND('',#4390,.T.);
#4839=FACE_BOUND('',#4391,.T.);
#4840=FACE_BOUND('',#4392,.T.);
#4841=FACE_BOUND('',#4393,.T.);
#4842=FACE_BOUND('',#4394,.T.);
#4843=FACE_BOUND('',#4395,.T.);
#4844=FACE_BOUND('',#4396,.T.);
#4845=FACE_BOUND('',#4397,.T.);
#4846=FACE_BOUND('',#4398,.T.);
#4847=FACE_BOUND('',#4399,.T.);
#4848=FACE_BOUND('',#4400,.T.);
#4849=FACE_BOUND('',#4401,.T.);
#4850=FACE_BOUND('',#4402,.T.);
#4851=FACE_BOUND('',#4403,.T.);
#4852=FACE_BOUND('',#4404,.T.);
#4853=FACE_BOUND('',#4405,.T.);
#4854=FACE_BOUND('',#4406,.T.);
#4855=FACE_BOUND('',#4407,.T.);
#4856=FACE_BOUND('',#4408,.T.);
#4857=FACE_BOUND('',#4409,.T.);
#4858=FACE_BOUND('',#4410,.T.);
#4859=FACE_BOUND('',#4411,.T.);
#4860=FACE_BOUND('',#4412,.T.);
#4861=FACE_BOUND('',#4413,.T.);
#4862=FACE_BOUND('',#4414,.T.);
#4863=FACE_BOUND('',#4415,.T.);
#4864=FACE_BOUND('',#4416,.T.);
#4865=FACE_BOUND('',#4417,.T.);
#4866=FACE_BOUND('',#4418,.T.);
#4867=FACE_BOUND('',#4419,.T.);
#4868=FACE_BOUND('',#4420,.T.);
#4869=FACE_BOUND('',#4421,.T.);
#4870=FACE_BOUND('',#4422,.T.);
#4871=FACE_BOUND('',#4423,.T.);
#4872=FACE_BOUND('',#4424,.T.);
#4873=FACE_BOUND('',#4425,.T.);
#4874=FACE_BOUND('',#4426,.T.);
#4875=FACE_BOUND('',#4427,.T.);
#4876=FACE_BOUND('',#4428,.T.);
#4877=FACE_BOUND('',#4429,.T.);
#4878=FACE_BOUND('',#4430,.T.);
#4879=FACE_BOUND('',#4431,.T.);
#4880=FACE_BOUND('',#4432,.T.);
#4881=FACE_BOUND('',#4433,.T.);
#4882=FACE_BOUND('',#4434,.T.);
#4883=FACE_BOUND('',#4435,.T.);
#4884=FACE_BOUND('',#4436,.T.);
#4885=FACE_BOUND('',#4437,.T.);
#4886=FACE_BOUND('',#4438,.T.);
#4887=FACE_BOUND('',#4439,.T.);
#4888=FACE_BOUND('',#4440,.T.);
#4889=FACE_BOUND('',#4441,.T.);
#4890=FACE_BOUND('',#4442,.T.);
#4891=FACE_BOUND('',#4443,.T.);
#4892=FACE_BOUND('',#4444,.T.);
#4893=FACE_BOUND('',#4445,.T.);
#4894=FACE_BOUND('',#4446,.T.);
#4895=FACE_BOUND('',#4447,.T.);
#4896=FACE_BOUND('',#4448,.T.);
#4897=FACE_BOUND('',#4449,.T.);
#4898=FACE_BOUND('',#4450,.T.);
#4899=FACE_BOUND('',#4451,.T.);
#5096=CYLINDRICAL_SURFACE('',#6074,0.0015);
#5097=CYLINDRICAL_SURFACE('',#6077,0.0025);
#5098=CYLINDRICAL_SURFACE('',#6169,0.006);
#5099=CYLINDRICAL_SURFACE('',#6171,0.006);
#5100=CYLINDRICAL_SURFACE('',#6173,0.006);
#5101=CYLINDRICAL_SURFACE('',#6175,0.006);
#5102=CYLINDRICAL_SURFACE('',#6177,0.006);
#5103=CYLINDRICAL_SURFACE('',#6179,0.006);
#5104=CYLINDRICAL_SURFACE('',#6181,0.006);
#5105=CYLINDRICAL_SURFACE('',#6183,0.006);
#5106=CYLINDRICAL_SURFACE('',#6185,0.006);
#5107=CYLINDRICAL_SURFACE('',#6187,0.006);
#5108=CYLINDRICAL_SURFACE('',#6189,0.006);
#5109=CYLINDRICAL_SURFACE('',#6191,0.006);
#5110=CYLINDRICAL_SURFACE('',#6193,0.006);
#5111=CYLINDRICAL_SURFACE('',#6195,0.006);
#5112=CYLINDRICAL_SURFACE('',#6197,0.006);
#5113=CYLINDRICAL_SURFACE('',#6199,0.006);
#5114=CYLINDRICAL_SURFACE('',#6201,0.006);
#5115=CYLINDRICAL_SURFACE('',#6203,0.006);
#5116=CYLINDRICAL_SURFACE('',#6205,0.006);
#5117=CYLINDRICAL_SURFACE('',#6207,0.006);
#5118=CYLINDRICAL_SURFACE('',#6209,0.006);
#5119=CYLINDRICAL_SURFACE('',#6279,0.006);
#5120=CYLINDRICAL_SURFACE('',#6280,0.0022);
#5121=CYLINDRICAL_SURFACE('',#6281,0.0022);
#5122=CYLINDRICAL_SURFACE('',#6282,0.004874);
#5123=CYLINDRICAL_SURFACE('',#6283,0.0022);
#5124=CYLINDRICAL_SURFACE('',#6284,0.0022);
#5125=CYLINDRICAL_SURFACE('',#6285,0.004874);
#5126=CYLINDRICAL_SURFACE('',#6286,0.0022);
#5127=CYLINDRICAL_SURFACE('',#6287,0.0022);
#5128=CYLINDRICAL_SURFACE('',#6288,0.004874);
#5129=CYLINDRICAL_SURFACE('',#6289,0.0022);
#5130=CYLINDRICAL_SURFACE('',#6290,0.0022);
#5131=CYLINDRICAL_SURFACE('',#6291,0.004874);
#5132=CYLINDRICAL_SURFACE('',#6292,0.0022);
#5133=CYLINDRICAL_SURFACE('',#6293,0.0022);
#5134=CYLINDRICAL_SURFACE('',#6294,0.004874);
#5135=CYLINDRICAL_SURFACE('',#6295,0.0022);
#5136=CYLINDRICAL_SURFACE('',#6296,0.0022);
#5137=CYLINDRICAL_SURFACE('',#6297,0.004874);
#5138=CYLINDRICAL_SURFACE('',#6298,0.0022);
#5139=CYLINDRICAL_SURFACE('',#6299,0.0022);
#5140=CYLINDRICAL_SURFACE('',#6300,0.004874);
#5141=CYLINDRICAL_SURFACE('',#6301,0.0022);
#5142=CYLINDRICAL_SURFACE('',#6302,0.0022);
#5143=CYLINDRICAL_SURFACE('',#6303,0.004874);
#5144=CYLINDRICAL_SURFACE('',#6304,0.0022);
#5145=CYLINDRICAL_SURFACE('',#6305,0.0022);
#5146=CYLINDRICAL_SURFACE('',#6306,0.004874);
#5147=CYLINDRICAL_SURFACE('',#6307,0.0022);
#5148=CYLINDRICAL_SURFACE('',#6308,0.0022);
#5149=CYLINDRICAL_SURFACE('',#6309,0.004874);
#5150=CYLINDRICAL_SURFACE('',#6310,0.0022);
#5151=CYLINDRICAL_SURFACE('',#6311,0.0022);
#5152=CYLINDRICAL_SURFACE('',#6312,0.004874);
#5153=CYLINDRICAL_SURFACE('',#6313,0.0022);
#5154=CYLINDRICAL_SURFACE('',#6314,0.0022);
#5155=CYLINDRICAL_SURFACE('',#6315,0.004874);
#5156=CYLINDRICAL_SURFACE('',#6316,0.0022);
#5157=CYLINDRICAL_SURFACE('',#6317,0.0022);
#5158=CYLINDRICAL_SURFACE('',#6318,0.004874);
#5159=CYLINDRICAL_SURFACE('',#6319,0.0022);
#5160=CYLINDRICAL_SURFACE('',#6320,0.0022);
#5161=CYLINDRICAL_SURFACE('',#6321,0.004874);
#5162=CYLINDRICAL_SURFACE('',#6322,0.0022);
#5163=CYLINDRICAL_SURFACE('',#6323,0.0022);
#5164=CYLINDRICAL_SURFACE('',#6324,0.004874);
#5165=CYLINDRICAL_SURFACE('',#6325,0.0022);
#5166=CYLINDRICAL_SURFACE('',#6326,0.0022);
#5167=CYLINDRICAL_SURFACE('',#6327,0.004874);
#5168=CYLINDRICAL_SURFACE('',#6328,0.0022);
#5169=CYLINDRICAL_SURFACE('',#6329,0.0022);
#5170=CYLINDRICAL_SURFACE('',#6330,0.004874);
#5171=CYLINDRICAL_SURFACE('',#6331,0.0022);
#5172=CYLINDRICAL_SURFACE('',#6332,0.0022);
#5173=CYLINDRICAL_SURFACE('',#6333,0.004874);
#5174=CYLINDRICAL_SURFACE('',#6334,0.0022);
#5175=CYLINDRICAL_SURFACE('',#6335,0.0022);
#5176=CYLINDRICAL_SURFACE('',#6336,0.004874);
#5177=CYLINDRICAL_SURFACE('',#6337,0.0022);
#5178=CYLINDRICAL_SURFACE('',#6338,0.0022);
#5179=CYLINDRICAL_SURFACE('',#6339,0.004874);
#5180=CYLINDRICAL_SURFACE('',#6340,0.0022);
#5181=CYLINDRICAL_SURFACE('',#6341,0.0022);
#5182=CYLINDRICAL_SURFACE('',#6342,0.004874);
#5183=CYLINDRICAL_SURFACE('',#6343,0.0022);
#5184=CYLINDRICAL_SURFACE('',#6344,0.0022);
#5185=CYLINDRICAL_SURFACE('',#6345,0.004874);
#5186=CYLINDRICAL_SURFACE('',#6351,0.00375738138352587);
#5187=CYLINDRICAL_SURFACE('',#6353,0.0015);
#5188=CYLINDRICAL_SURFACE('',#6358,0.0025);
#5371=ADVANCED_FACE('',(#4790,#4791),#5096,.F.);
#5372=ADVANCED_FACE('',(#4792,#4793),#5097,.T.);
#5373=ADVANCED_FACE('',(#4794,#4795),#757,.F.);
#5374=ADVANCED_FACE('',(#4796),#5098,.T.);
#5375=ADVANCED_FACE('',(#4797),#5099,.T.);
#5376=ADVANCED_FACE('',(#4798),#5100,.T.);
#5377=ADVANCED_FACE('',(#4799),#5101,.T.);
#5378=ADVANCED_FACE('',(#4800),#5102,.T.);
#5379=ADVANCED_FACE('',(#4801),#5103,.T.);
#5380=ADVANCED_FACE('',(#4802),#5104,.T.);
#5381=ADVANCED_FACE('',(#4803),#5105,.T.);
#5382=ADVANCED_FACE('',(#4804),#5106,.T.);
#5383=ADVANCED_FACE('',(#4805),#5107,.T.);
#5384=ADVANCED_FACE('',(#4806),#5108,.T.);
#5385=ADVANCED_FACE('',(#4807),#5109,.T.);
#5386=ADVANCED_FACE('',(#4808),#5110,.T.);
#5387=ADVANCED_FACE('',(#4809),#5111,.T.);
#5388=ADVANCED_FACE('',(#4810),#5112,.T.);
#5389=ADVANCED_FACE('',(#4811),#5113,.T.);
#5390=ADVANCED_FACE('',(#4812),#5114,.T.);
#5391=ADVANCED_FACE('',(#4813),#5115,.T.);
#5392=ADVANCED_FACE('',(#4814),#5116,.T.);
#5393=ADVANCED_FACE('',(#4815),#5117,.T.);
#5394=ADVANCED_FACE('',(#4816),#5118,.T.);
#5395=ADVANCED_FACE('',(#4817,#4818),#758,.F.);
#5396=ADVANCED_FACE('',(#4819),#5119,.T.);
#5397=ADVANCED_FACE('',(#4820),#5120,.T.);
#5398=ADVANCED_FACE('',(#4821),#5121,.T.);
#5399=ADVANCED_FACE('',(#4822),#5122,.T.);
#5400=ADVANCED_FACE('',(#4823),#5123,.T.);
#5401=ADVANCED_FACE('',(#4824),#5124,.T.);
#5402=ADVANCED_FACE('',(#4825),#5125,.T.);
#5403=ADVANCED_FACE('',(#4826),#5126,.T.);
#5404=ADVANCED_FACE('',(#4827),#5127,.T.);
#5405=ADVANCED_FACE('',(#4828),#5128,.T.);
#5406=ADVANCED_FACE('',(#4829),#5129,.T.);
#5407=ADVANCED_FACE('',(#4830),#5130,.T.);
#5408=ADVANCED_FACE('',(#4831),#5131,.T.);
#5409=ADVANCED_FACE('',(#4832),#5132,.T.);
#5410=ADVANCED_FACE('',(#4833),#5133,.T.);
#5411=ADVANCED_FACE('',(#4834),#5134,.T.);
#5412=ADVANCED_FACE('',(#4835),#5135,.T.);
#5413=ADVANCED_FACE('',(#4836),#5136,.T.);
#5414=ADVANCED_FACE('',(#4837),#5137,.T.);
#5415=ADVANCED_FACE('',(#4838),#5138,.T.);
#5416=ADVANCED_FACE('',(#4839),#5139,.T.);
#5417=ADVANCED_FACE('',(#4840),#5140,.T.);
#5418=ADVANCED_FACE('',(#4841),#5141,.T.);
#5419=ADVANCED_FACE('',(#4842),#5142,.T.);
#5420=ADVANCED_FACE('',(#4843),#5143,.T.);
#5421=ADVANCED_FACE('',(#4844),#5144,.T.);
#5422=ADVANCED_FACE('',(#4845),#5145,.T.);
#5423=ADVANCED_FACE('',(#4846),#5146,.T.);
#5424=ADVANCED_FACE('',(#4847),#5147,.T.);
#5425=ADVANCED_FACE('',(#4848),#5148,.T.);
#5426=ADVANCED_FACE('',(#4849),#5149,.T.);
#5427=ADVANCED_FACE('',(#4850),#5150,.T.);
#5428=ADVANCED_FACE('',(#4851),#5151,.T.);
#5429=ADVANCED_FACE('',(#4852),#5152,.T.);
#5430=ADVANCED_FACE('',(#4853),#5153,.T.);
#5431=ADVANCED_FACE('',(#4854),#5154,.T.);
#5432=ADVANCED_FACE('',(#4855),#5155,.T.);
#5433=ADVANCED_FACE('',(#4856),#5156,.T.);
#5434=ADVANCED_FACE('',(#4857),#5157,.T.);
#5435=ADVANCED_FACE('',(#4858),#5158,.T.);
#5436=ADVANCED_FACE('',(#4859),#5159,.T.);
#5437=ADVANCED_FACE('',(#4860),#5160,.T.);
#5438=ADVANCED_FACE('',(#4861),#5161,.T.);
#5439=ADVANCED_FACE('',(#4862),#5162,.T.);
#5440=ADVANCED_FACE('',(#4863),#5163,.T.);
#5441=ADVANCED_FACE('',(#4864),#5164,.T.);
#5442=ADVANCED_FACE('',(#4865),#5165,.T.);
#5443=ADVANCED_FACE('',(#4866),#5166,.T.);
#5444=ADVANCED_FACE('',(#4867),#5167,.T.);
#5445=ADVANCED_FACE('',(#4868),#5168,.T.);
#5446=ADVANCED_FACE('',(#4869),#5169,.T.);
#5447=ADVANCED_FACE('',(#4870),#5170,.T.);
#5448=ADVANCED_FACE('',(#4871),#5171,.T.);
#5449=ADVANCED_FACE('',(#4872),#5172,.T.);
#5450=ADVANCED_FACE('',(#4873),#5173,.T.);
#5451=ADVANCED_FACE('',(#4874),#5174,.T.);
#5452=ADVANCED_FACE('',(#4875),#5175,.T.);
#5453=ADVANCED_FACE('',(#4876),#5176,.T.);
#5454=ADVANCED_FACE('',(#4877),#5177,.T.);
#5455=ADVANCED_FACE('',(#4878),#5178,.T.);
#5456=ADVANCED_FACE('',(#4879),#5179,.T.);
#5457=ADVANCED_FACE('',(#4880),#5180,.T.);
#5458=ADVANCED_FACE('',(#4881),#5181,.T.);
#5459=ADVANCED_FACE('',(#4882),#5182,.T.);
#5460=ADVANCED_FACE('',(#4883),#5183,.T.);
#5461=ADVANCED_FACE('',(#4884),#5184,.T.);
#5462=ADVANCED_FACE('',(#4885),#5185,.T.);
#5463=ADVANCED_FACE('',(#4886,#4887),#759,.T.);
#5464=ADVANCED_FACE('',(#4888,#4889),#760,.F.);
#5465=ADVANCED_FACE('',(#4890,#4891),#5186,.T.);
#5466=ADVANCED_FACE('',(#4892),#761,.F.);
#5467=ADVANCED_FACE('',(#4893,#4894),#5187,.F.);
#5468=ADVANCED_FACE('',(#4895,#4896),#762,.T.);
#5469=ADVANCED_FACE('',(#4897,#4898),#5188,.T.);
#5470=ADVANCED_FACE('',(#4899),#763,.T.);
#5546=CLOSED_SHELL('',(#5371,#5372,#5373,#5374,#5375,#5376,#5377,#5378,
#5379,#5380,#5381,#5382,#5383,#5384,#5385,#5386,#5387,#5388,#5389,#5390,
#5391,#5392,#5393,#5394,#5395,#5396,#5397,#5398,#5399,#5400,#5401,#5402,
#5403,#5404,#5405,#5406,#5407,#5408,#5409,#5410,#5411,#5412,#5413,#5414,
#5415,#5416,#5417,#5418,#5419,#5420,#5421,#5422,#5423,#5424,#5425,#5426,
#5427,#5428,#5429,#5430,#5431,#5432,#5433,#5434,#5435,#5436,#5437,#5438,
#5439,#5440,#5441,#5442,#5443,#5444,#5445,#5446,#5447,#5448,#5449,#5450,
#5451,#5452,#5453,#5454,#5455,#5456,#5457,#5458,#5459,#5460,#5461,#5462,
#5463,#5464,#5465,#5466,#5467,#5468,#5469,#5470));
#5560=STYLED_ITEM('',(#5574),#5665);
#5574=PRESENTATION_STYLE_ASSIGNMENT((#5588));
#5588=SURFACE_STYLE_USAGE(.BOTH.,#5602);
#5602=SURFACE_SIDE_STYLE('',(#5616));
#5616=SURFACE_STYLE_FILL_AREA(#5630);
#5630=FILL_AREA_STYLE('',(#5644));
#5644=FILL_AREA_STYLE_COLOUR('',#5655);
#5655=COLOUR_RGB('', 0.31764706, 0.68627451, 0.89019608);
#5665=MANIFOLD_SOLID_BREP('Part 1',#5546);
#5680=SHAPE_DEFINITION_REPRESENTATION(#10194,#5696);
#5696=SHAPE_REPRESENTATION('Part 1',(#5704),#10150);
#5704=AXIS2_PLACEMENT_3D('',#8391,#6505,#6506);
#6074=AXIS2_PLACEMENT_3D('',#9234,#7394,#7395);
#6075=AXIS2_PLACEMENT_3D('',#9235,#7396,#7397);
#6076=AXIS2_PLACEMENT_3D('',#9237,#7398,#7399);
#6077=AXIS2_PLACEMENT_3D('',#9239,#7400,#7401);
#6078=AXIS2_PLACEMENT_3D('',#9240,#7402,#7403);
#6079=AXIS2_PLACEMENT_3D('',#9242,#7404,#7405);
#6080=AXIS2_PLACEMENT_3D('',#9244,#7406,#7407);
#6081=AXIS2_PLACEMENT_3D('',#9245,#7408,#7409);
#6082=AXIS2_PLACEMENT_3D('',#9248,#7410,#7411);
#6083=AXIS2_PLACEMENT_3D('',#9250,#7412,#7413);
#6084=AXIS2_PLACEMENT_3D('',#9252,#7414,#7415);
#6085=AXIS2_PLACEMENT_3D('',#9254,#7416,#7417);
#6086=AXIS2_PLACEMENT_3D('',#9256,#7418,#7419);
#6087=AXIS2_PLACEMENT_3D('',#9258,#7420,#7421);
#6088=AXIS2_PLACEMENT_3D('',#9260,#7422,#7423);
#6089=AXIS2_PLACEMENT_3D('',#9262,#7424,#7425);
#6090=AXIS2_PLACEMENT_3D('',#9264,#7426,#7427);
#6091=AXIS2_PLACEMENT_3D('',#9266,#7428,#7429);
#6092=AXIS2_PLACEMENT_3D('',#9268,#7430,#7431);
#6093=AXIS2_PLACEMENT_3D('',#9270,#7432,#7433);
#6094=AXIS2_PLACEMENT_3D('',#9272,#7434,#7435);
#6095=AXIS2_PLACEMENT_3D('',#9274,#7436,#7437);
#6096=AXIS2_PLACEMENT_3D('',#9276,#7438,#7439);
#6097=AXIS2_PLACEMENT_3D('',#9278,#7440,#7441);
#6098=AXIS2_PLACEMENT_3D('',#9280,#7442,#7443);
#6099=AXIS2_PLACEMENT_3D('',#9282,#7444,#7445);
#6100=AXIS2_PLACEMENT_3D('',#9284,#7446,#7447);
#6101=AXIS2_PLACEMENT_3D('',#9286,#7448,#7449);
#6102=AXIS2_PLACEMENT_3D('',#9288,#7450,#7451);
#6103=AXIS2_PLACEMENT_3D('',#9290,#7452,#7453);
#6104=AXIS2_PLACEMENT_3D('',#9292,#7454,#7455);
#6105=AXIS2_PLACEMENT_3D('',#9294,#7456,#7457);
#6106=AXIS2_PLACEMENT_3D('',#9296,#7458,#7459);
#6107=AXIS2_PLACEMENT_3D('',#9298,#7460,#7461);
#6108=AXIS2_PLACEMENT_3D('',#9300,#7462,#7463);
#6109=AXIS2_PLACEMENT_3D('',#9302,#7464,#7465);
#6110=AXIS2_PLACEMENT_3D('',#9304,#7466,#7467);
#6111=AXIS2_PLACEMENT_3D('',#9306,#7468,#7469);
#6112=AXIS2_PLACEMENT_3D('',#9308,#7470,#7471);
#6113=AXIS2_PLACEMENT_3D('',#9310,#7472,#7473);
#6114=AXIS2_PLACEMENT_3D('',#9312,#7474,#7475);
#6115=AXIS2_PLACEMENT_3D('',#9314,#7476,#7477);
#6116=AXIS2_PLACEMENT_3D('',#9316,#7478,#7479);
#6117=AXIS2_PLACEMENT_3D('',#9318,#7480,#7481);
#6118=AXIS2_PLACEMENT_3D('',#9320,#7482,#7483);
#6119=AXIS2_PLACEMENT_3D('',#9322,#7484,#7485);
#6120=AXIS2_PLACEMENT_3D('',#9324,#7486,#7487);
#6121=AXIS2_PLACEMENT_3D('',#9326,#7488,#7489);
#6122=AXIS2_PLACEMENT_3D('',#9328,#7490,#7491);
#6123=AXIS2_PLACEMENT_3D('',#9330,#7492,#7493);
#6124=AXIS2_PLACEMENT_3D('',#9332,#7494,#7495);
#6125=AXIS2_PLACEMENT_3D('',#9334,#7496,#7497);
#6126=AXIS2_PLACEMENT_3D('',#9336,#7498,#7499);
#6127=AXIS2_PLACEMENT_3D('',#9338,#7500,#7501);
#6128=AXIS2_PLACEMENT_3D('',#9340,#7502,#7503);
#6129=AXIS2_PLACEMENT_3D('',#9342,#7504,#7505);
#6130=AXIS2_PLACEMENT_3D('',#9344,#7506,#7507);
#6131=AXIS2_PLACEMENT_3D('',#9346,#7508,#7509);
#6132=AXIS2_PLACEMENT_3D('',#9348,#7510,#7511);
#6133=AXIS2_PLACEMENT_3D('',#9350,#7512,#7513);
#6134=AXIS2_PLACEMENT_3D('',#9352,#7514,#7515);
#6135=AXIS2_PLACEMENT_3D('',#9354,#7516,#7517);
#6136=AXIS2_PLACEMENT_3D('',#9356,#7518,#7519);
#6137=AXIS2_PLACEMENT_3D('',#9358,#7520,#7521);
#6138=AXIS2_PLACEMENT_3D('',#9360,#7522,#7523);
#6139=AXIS2_PLACEMENT_3D('',#9362,#7524,#7525);
#6140=AXIS2_PLACEMENT_3D('',#9364,#7526,#7527);
#6141=AXIS2_PLACEMENT_3D('',#9366,#7528,#7529);
#6142=AXIS2_PLACEMENT_3D('',#9368,#7530,#7531);
#6143=AXIS2_PLACEMENT_3D('',#9370,#7532,#7533);
#6144=AXIS2_PLACEMENT_3D('',#9372,#7534,#7535);
#6145=AXIS2_PLACEMENT_3D('',#9374,#7536,#7537);
#6146=AXIS2_PLACEMENT_3D('',#9376,#7538,#7539);
#6147=AXIS2_PLACEMENT_3D('',#9378,#7540,#7541);
#6148=AXIS2_PLACEMENT_3D('',#9380,#7542,#7543);
#6149=AXIS2_PLACEMENT_3D('',#9382,#7544,#7545);
#6150=AXIS2_PLACEMENT_3D('',#9384,#7546,#7547);
#6151=AXIS2_PLACEMENT_3D('',#9386,#7548,#7549);
#6152=AXIS2_PLACEMENT_3D('',#9388,#7550,#7551);
#6153=AXIS2_PLACEMENT_3D('',#9390,#7552,#7553);
#6154=AXIS2_PLACEMENT_3D('',#9392,#7554,#7555);
#6155=AXIS2_PLACEMENT_3D('',#9394,#7556,#7557);
#6156=AXIS2_PLACEMENT_3D('',#9396,#7558,#7559);
#6157=AXIS2_PLACEMENT_3D('',#9398,#7560,#7561);
#6158=AXIS2_PLACEMENT_3D('',#9400,#7562,#7563);
#6159=AXIS2_PLACEMENT_3D('',#9402,#7564,#7565);
#6160=AXIS2_PLACEMENT_3D('',#9404,#7566,#7567);
#6161=AXIS2_PLACEMENT_3D('',#9406,#7568,#7569);
#6162=AXIS2_PLACEMENT_3D('',#9408,#7570,#7571);
#6163=AXIS2_PLACEMENT_3D('',#9410,#7572,#7573);
#6164=AXIS2_PLACEMENT_3D('',#9412,#7574,#7575);
#6165=AXIS2_PLACEMENT_3D('',#9414,#7576,#7577);
#6166=AXIS2_PLACEMENT_3D('',#9416,#7578,#7579);
#6167=AXIS2_PLACEMENT_3D('',#9418,#7580,#7581);
#6168=AXIS2_PLACEMENT_3D('',#9420,#7582,#7583);
#6169=AXIS2_PLACEMENT_3D('',#9421,#7584,#7585);
#6170=AXIS2_PLACEMENT_3D('',#9426,#7588,#7589);
#6171=AXIS2_PLACEMENT_3D('',#9427,#7590,#7591);
#6172=AXIS2_PLACEMENT_3D('',#9430,#7593,#7594);
#6173=AXIS2_PLACEMENT_3D('',#9433,#7596,#7597);
#6174=AXIS2_PLACEMENT_3D('',#9438,#7600,#7601);
#6175=AXIS2_PLACEMENT_3D('',#9439,#7602,#7603);
#6176=AXIS2_PLACEMENT_3D('',#9444,#7606,#7607);
#6177=AXIS2_PLACEMENT_3D('',#9445,#7608,#7609);
#6178=AXIS2_PLACEMENT_3D('',#9450,#7612,#7613);
#6179=AXIS2_PLACEMENT_3D('',#9451,#7614,#7615);
#6180=AXIS2_PLACEMENT_3D('',#9454,#7617,#7618);
#6181=AXIS2_PLACEMENT_3D('',#9457,#7620,#7621);
#6182=AXIS2_PLACEMENT_3D('',#9462,#7624,#7625);
#6183=AXIS2_PLACEMENT_3D('',#9463,#7626,#7627);
#6184=AXIS2_PLACEMENT_3D('',#9466,#7629,#7630);
#6185=AXIS2_PLACEMENT_3D('',#9469,#7632,#7633);
#6186=AXIS2_PLACEMENT_3D('',#9474,#7636,#7637);
#6187=AXIS2_PLACEMENT_3D('',#9475,#7638,#7639);
#6188=AXIS2_PLACEMENT_3D('',#9480,#7642,#7643);
#6189=AXIS2_PLACEMENT_3D('',#9481,#7644,#7645);
#6190=AXIS2_PLACEMENT_3D('',#9484,#7647,#7648);
#6191=AXIS2_PLACEMENT_3D('',#9487,#7650,#7651);
#6192=AXIS2_PLACEMENT_3D('',#9492,#7654,#7655);
#6193=AXIS2_PLACEMENT_3D('',#9493,#7656,#7657);
#6194=AXIS2_PLACEMENT_3D('',#9496,#7659,#7660);
#6195=AXIS2_PLACEMENT_3D('',#9499,#7662,#7663);
#6196=AXIS2_PLACEMENT_3D('',#9502,#7665,#7666);
#6197=AXIS2_PLACEMENT_3D('',#9505,#7668,#7669);
#6198=AXIS2_PLACEMENT_3D('',#9508,#7671,#7672);
#6199=AXIS2_PLACEMENT_3D('',#9511,#7674,#7675);
#6200=AXIS2_PLACEMENT_3D('',#9516,#7678,#7679);
#6201=AXIS2_PLACEMENT_3D('',#9517,#7680,#7681);
#6202=AXIS2_PLACEMENT_3D('',#9522,#7684,#7685);
#6203=AXIS2_PLACEMENT_3D('',#9523,#7686,#7687);
#6204=AXIS2_PLACEMENT_3D('',#9526,#7689,#7690);
#6205=AXIS2_PLACEMENT_3D('',#9529,#7692,#7693);
#6206=AXIS2_PLACEMENT_3D('',#9532,#7695,#7696);
#6207=AXIS2_PLACEMENT_3D('',#9535,#7698,#7699);
#6208=AXIS2_PLACEMENT_3D('',#9538,#7701,#7702);
#6209=AXIS2_PLACEMENT_3D('',#9541,#7704,#7705);
#6210=AXIS2_PLACEMENT_3D('',#9546,#7708,#7709);
#6211=AXIS2_PLACEMENT_3D('',#9547,#7710,#7711);
#6212=AXIS2_PLACEMENT_3D('',#9548,#7712,#7713);
#6213=AXIS2_PLACEMENT_3D('',#9550,#7714,#7715);
#6214=AXIS2_PLACEMENT_3D('',#9552,#7716,#7717);
#6215=AXIS2_PLACEMENT_3D('',#9554,#7718,#7719);
#6216=AXIS2_PLACEMENT_3D('',#9555,#7720,#7721);
#6217=AXIS2_PLACEMENT_3D('',#9557,#7722,#7723);
#6218=AXIS2_PLACEMENT_3D('',#9559,#7724,#7725);
#6219=AXIS2_PLACEMENT_3D('',#9560,#7726,#7727);
#6220=AXIS2_PLACEMENT_3D('',#9562,#7728,#7729);
#6221=AXIS2_PLACEMENT_3D('',#9564,#7730,#7731);
#6222=AXIS2_PLACEMENT_3D('',#9565,#7732,#7733);
#6223=AXIS2_PLACEMENT_3D('',#9567,#7734,#7735);
#6224=AXIS2_PLACEMENT_3D('',#9569,#7736,#7737);
#6225=AXIS2_PLACEMENT_3D('',#9570,#7738,#7739);
#6226=AXIS2_PLACEMENT_3D('',#9572,#7740,#7741);
#6227=AXIS2_PLACEMENT_3D('',#9574,#7742,#7743);
#6228=AXIS2_PLACEMENT_3D('',#9576,#7744,#7745);
#6229=AXIS2_PLACEMENT_3D('',#9578,#7746,#7747);
#6230=AXIS2_PLACEMENT_3D('',#9580,#7748,#7749);
#6231=AXIS2_PLACEMENT_3D('',#9582,#7750,#7751);
#6232=AXIS2_PLACEMENT_3D('',#9583,#7752,#7753);
#6233=AXIS2_PLACEMENT_3D('',#9585,#7754,#7755);
#6234=AXIS2_PLACEMENT_3D('',#9587,#7756,#7757);
#6235=AXIS2_PLACEMENT_3D('',#9588,#7758,#7759);
#6236=AXIS2_PLACEMENT_3D('',#9590,#7760,#7761);
#6237=AXIS2_PLACEMENT_3D('',#9592,#7762,#7763);
#6238=AXIS2_PLACEMENT_3D('',#9593,#7764,#7765);
#6239=AXIS2_PLACEMENT_3D('',#9595,#7766,#7767);
#6240=AXIS2_PLACEMENT_3D('',#9597,#7768,#7769);
#6241=AXIS2_PLACEMENT_3D('',#9598,#7770,#7771);
#6242=AXIS2_PLACEMENT_3D('',#9600,#7772,#7773);
#6243=AXIS2_PLACEMENT_3D('',#9602,#7774,#7775);
#6244=AXIS2_PLACEMENT_3D('',#9603,#7776,#7777);
#6245=AXIS2_PLACEMENT_3D('',#9605,#7778,#7779);
#6246=AXIS2_PLACEMENT_3D('',#9607,#7780,#7781);
#6247=AXIS2_PLACEMENT_3D('',#9608,#7782,#7783);
#6248=AXIS2_PLACEMENT_3D('',#9610,#7784,#7785);
#6249=AXIS2_PLACEMENT_3D('',#9612,#7786,#7787);
#6250=AXIS2_PLACEMENT_3D('',#9613,#7788,#7789);
#6251=AXIS2_PLACEMENT_3D('',#9615,#7790,#7791);
#6252=AXIS2_PLACEMENT_3D('',#9617,#7792,#7793);
#6253=AXIS2_PLACEMENT_3D('',#9618,#7794,#7795);
#6254=AXIS2_PLACEMENT_3D('',#9620,#7796,#7797);
#6255=AXIS2_PLACEMENT_3D('',#9622,#7798,#7799);
#6256=AXIS2_PLACEMENT_3D('',#9623,#7800,#7801);
#6257=AXIS2_PLACEMENT_3D('',#9625,#7802,#7803);
#6258=AXIS2_PLACEMENT_3D('',#9627,#7804,#7805);
#6259=AXIS2_PLACEMENT_3D('',#9628,#7806,#7807);
#6260=AXIS2_PLACEMENT_3D('',#9630,#7808,#7809);
#6261=AXIS2_PLACEMENT_3D('',#9632,#7810,#7811);
#6262=AXIS2_PLACEMENT_3D('',#9633,#7812,#7813);
#6263=AXIS2_PLACEMENT_3D('',#9635,#7814,#7815);
#6264=AXIS2_PLACEMENT_3D('',#9637,#7816,#7817);
#6265=AXIS2_PLACEMENT_3D('',#9638,#7818,#7819);
#6266=AXIS2_PLACEMENT_3D('',#9640,#7820,#7821);
#6267=AXIS2_PLACEMENT_3D('',#9642,#7822,#7823);
#6268=AXIS2_PLACEMENT_3D('',#9643,#7824,#7825);
#6269=AXIS2_PLACEMENT_3D('',#9645,#7826,#7827);
#6270=AXIS2_PLACEMENT_3D('',#9647,#7828,#7829);
#6271=AXIS2_PLACEMENT_3D('',#9648,#7830,#7831);
#6272=AXIS2_PLACEMENT_3D('',#9650,#7832,#7833);
#6273=AXIS2_PLACEMENT_3D('',#9652,#7834,#7835);
#6274=AXIS2_PLACEMENT_3D('',#9653,#7836,#7837);
#6275=AXIS2_PLACEMENT_3D('',#9655,#7838,#7839);
#6276=AXIS2_PLACEMENT_3D('',#9657,#7840,#7841);
#6277=AXIS2_PLACEMENT_3D('',#9658,#7842,#7843);
#6278=AXIS2_PLACEMENT_3D('',#9660,#7844,#7845);
#6279=AXIS2_PLACEMENT_3D('',#9661,#7846,#7847);
#6280=AXIS2_PLACEMENT_3D('',#9664,#7850,#7851);
#6281=AXIS2_PLACEMENT_3D('',#9666,#7853,#7854);
#6282=AXIS2_PLACEMENT_3D('',#9668,#7856,#7857);
#6283=AXIS2_PLACEMENT_3D('',#9669,#7858,#7859);
#6284=AXIS2_PLACEMENT_3D('',#9671,#7861,#7862);
#6285=AXIS2_PLACEMENT_3D('',#9673,#7864,#7865);
#6286=AXIS2_PLACEMENT_3D('',#9674,#7866,#7867);
#6287=AXIS2_PLACEMENT_3D('',#9676,#7869,#7870);
#6288=AXIS2_PLACEMENT_3D('',#9678,#7872,#7873);
#6289=AXIS2_PLACEMENT_3D('',#9679,#7874,#7875);
#6290=AXIS2_PLACEMENT_3D('',#9681,#7877,#7878);
#6291=AXIS2_PLACEMENT_3D('',#9683,#7880,#7881);
#6292=AXIS2_PLACEMENT_3D('',#9684,#7882,#7883);
#6293=AXIS2_PLACEMENT_3D('',#9686,#7885,#7886);
#6294=AXIS2_PLACEMENT_3D('',#9688,#7888,#7889);
#6295=AXIS2_PLACEMENT_3D('',#9689,#7890,#7891);
#6296=AXIS2_PLACEMENT_3D('',#9691,#7893,#7894);
#6297=AXIS2_PLACEMENT_3D('',#9693,#7896,#7897);
#6298=AXIS2_PLACEMENT_3D('',#9694,#7898,#7899);
#6299=AXIS2_PLACEMENT_3D('',#9696,#7901,#7902);
#6300=AXIS2_PLACEMENT_3D('',#9698,#7904,#7905);
#6301=AXIS2_PLACEMENT_3D('',#9699,#7906,#7907);
#6302=AXIS2_PLACEMENT_3D('',#9701,#7909,#7910);
#6303=AXIS2_PLACEMENT_3D('',#9703,#7912,#7913);
#6304=AXIS2_PLACEMENT_3D('',#9704,#7914,#7915);
#6305=AXIS2_PLACEMENT_3D('',#9706,#7917,#7918);
#6306=AXIS2_PLACEMENT_3D('',#9708,#7920,#7921);
#6307=AXIS2_PLACEMENT_3D('',#9709,#7922,#7923);
#6308=AXIS2_PLACEMENT_3D('',#9711,#7925,#7926);
#6309=AXIS2_PLACEMENT_3D('',#9713,#7928,#7929);
#6310=AXIS2_PLACEMENT_3D('',#9714,#7930,#7931);
#6311=AXIS2_PLACEMENT_3D('',#9716,#7933,#7934);
#6312=AXIS2_PLACEMENT_3D('',#9718,#7936,#7937);
#6313=AXIS2_PLACEMENT_3D('',#9719,#7938,#7939);
#6314=AXIS2_PLACEMENT_3D('',#9721,#7941,#7942);
#6315=AXIS2_PLACEMENT_3D('',#9723,#7944,#7945);
#6316=AXIS2_PLACEMENT_3D('',#9724,#7946,#7947);
#6317=AXIS2_PLACEMENT_3D('',#9726,#7949,#7950);
#6318=AXIS2_PLACEMENT_3D('',#9728,#7952,#7953);
#6319=AXIS2_PLACEMENT_3D('',#9729,#7954,#7955);
#6320=AXIS2_PLACEMENT_3D('',#9731,#7957,#7958);
#6321=AXIS2_PLACEMENT_3D('',#9733,#7960,#7961);
#6322=AXIS2_PLACEMENT_3D('',#9734,#7962,#7963);
#6323=AXIS2_PLACEMENT_3D('',#9736,#7965,#7966);
#6324=AXIS2_PLACEMENT_3D('',#9738,#7968,#7969);
#6325=AXIS2_PLACEMENT_3D('',#9739,#7970,#7971);
#6326=AXIS2_PLACEMENT_3D('',#9741,#7973,#7974);
#6327=AXIS2_PLACEMENT_3D('',#9743,#7976,#7977);
#6328=AXIS2_PLACEMENT_3D('',#9744,#7978,#7979);
#6329=AXIS2_PLACEMENT_3D('',#9746,#7981,#7982);
#6330=AXIS2_PLACEMENT_3D('',#9748,#7984,#7985);
#6331=AXIS2_PLACEMENT_3D('',#9749,#7986,#7987);
#6332=AXIS2_PLACEMENT_3D('',#9751,#7989,#7990);
#6333=AXIS2_PLACEMENT_3D('',#9753,#7992,#7993);
#6334=AXIS2_PLACEMENT_3D('',#9754,#7994,#7995);
#6335=AXIS2_PLACEMENT_3D('',#9756,#7997,#7998);
#6336=AXIS2_PLACEMENT_3D('',#9758,#8000,#8001);
#6337=AXIS2_PLACEMENT_3D('',#9759,#8002,#8003);
#6338=AXIS2_PLACEMENT_3D('',#9761,#8005,#8006);
#6339=AXIS2_PLACEMENT_3D('',#9763,#8008,#8009);
#6340=AXIS2_PLACEMENT_3D('',#9764,#8010,#8011);
#6341=AXIS2_PLACEMENT_3D('',#9766,#8013,#8014);
#6342=AXIS2_PLACEMENT_3D('',#9768,#8016,#8017);
#6343=AXIS2_PLACEMENT_3D('',#9769,#8018,#8019);
#6344=AXIS2_PLACEMENT_3D('',#9771,#8021,#8022);
#6345=AXIS2_PLACEMENT_3D('',#9773,#8024,#8025);
#6346=AXIS2_PLACEMENT_3D('',#9774,#8026,#8027);
#6347=AXIS2_PLACEMENT_3D('',#9775,#8028,#8029);
#6348=AXIS2_PLACEMENT_3D('',#9777,#8030,#8031);
#6349=AXIS2_PLACEMENT_3D('',#9779,#8032,#8033);
#6350=AXIS2_PLACEMENT_3D('',#9780,#8034,#8035);
#6351=AXIS2_PLACEMENT_3D('',#9782,#8036,#8037);
#6352=AXIS2_PLACEMENT_3D('',#9783,#8038,#8039);
#6353=AXIS2_PLACEMENT_3D('',#9784,#8040,#8041);
#6354=AXIS2_PLACEMENT_3D('',#9785,#8042,#8043);
#6355=AXIS2_PLACEMENT_3D('',#9787,#8044,#8045);
#6356=AXIS2_PLACEMENT_3D('',#9789,#8046,#8047);
#6357=AXIS2_PLACEMENT_3D('',#9790,#8048,#8049);
#6358=AXIS2_PLACEMENT_3D('',#9792,#8050,#8051);
#6359=AXIS2_PLACEMENT_3D('',#9793,#8052,#8053);
#6505=DIRECTION('',(0.,0.,1.));
#6506=DIRECTION('',(1.,0.,0.));
#7394=DIRECTION('',(-1.,0.,0.));
#7395=DIRECTION('',(0.,0.,1.));
#7396=DIRECTION('',(1.,0.,0.));
#7397=DIRECTION('',(0.,0.,-1.));
#7398=DIRECTION('',(1.,0.,0.));
#7399=DIRECTION('',(0.,0.,-1.));
#7400=DIRECTION('',(-1.,0.,0.));
#7401=DIRECTION('',(0.,0.,1.));
#7402=DIRECTION('',(-1.,0.,0.));
#7403=DIRECTION('',(0.,0.,1.));
#7404=DIRECTION('',(1.,0.,0.));
#7405=DIRECTION('',(0.,0.,-1.));
#7406=DIRECTION('',(-1.,0.,0.));
#7407=DIRECTION('',(0.,0.,1.));
#7408=DIRECTION('',(-1.,0.,0.));
#7409=DIRECTION('',(0.,0.989821441880932,0.142314838273289));
#7410=DIRECTION('',(-1.,0.,0.));
#7411=DIRECTION('',(0.,0.989821441880932,0.142314838273289));
#7412=DIRECTION('',(-1.,0.,0.));
#7413=DIRECTION('',(0.,0.989821441880932,0.142314838273289));
#7414=DIRECTION('',(-1.,0.,0.));
#7415=DIRECTION('',(0.,0.,1.));
#7416=DIRECTION('',(-1.,0.,0.));
#7417=DIRECTION('',(0.,0.909631995354517,0.41541501300189));
#7418=DIRECTION('',(-1.,0.,0.));
#7419=DIRECTION('',(0.,0.909631995354517,0.41541501300189));
#7420=DIRECTION('',(-1.,0.,0.));
#7421=DIRECTION('',(0.,0.909631995354517,0.41541501300189));
#7422=DIRECTION('',(-1.,0.,0.));
#7423=DIRECTION('',(0.,0.,1.));
#7424=DIRECTION('',(-1.,0.,0.));
#7425=DIRECTION('',(0.,0.755749574354255,0.654860733945289));
#7426=DIRECTION('',(-1.,0.,0.));
#7427=DIRECTION('',(0.,0.755749574354255,0.654860733945289));
#7428=DIRECTION('',(-1.,0.,0.));
#7429=DIRECTION('',(0.,0.755749574354255,0.654860733945289));
#7430=DIRECTION('',(-1.,0.,0.));
#7431=DIRECTION('',(0.,0.,1.));
#7432=DIRECTION('',(-1.,0.,0.));
#7433=DIRECTION('',(0.,0.540640817455593,0.841253532831184));
#7434=DIRECTION('',(-1.,0.,0.));
#7435=DIRECTION('',(0.,0.540640817455593,0.841253532831184));
#7436=DIRECTION('',(-1.,0.,0.));
#7437=DIRECTION('',(0.,0.540640817455593,0.841253532831184));
#7438=DIRECTION('',(-1.,0.,0.));
#7439=DIRECTION('',(0.,0.,1.));
#7440=DIRECTION('',(-1.,0.,0.));
#7441=DIRECTION('',(0.,0.281732556841424,0.959492973614499));
#7442=DIRECTION('',(-1.,0.,0.));
#7443=DIRECTION('',(0.,0.281732556841424,0.959492973614499));
#7444=DIRECTION('',(-1.,0.,0.));
#7445=DIRECTION('',(0.,0.281732556841424,0.959492973614499));
#7446=DIRECTION('',(-1.,0.,0.));
#7447=DIRECTION('',(0.,0.,1.));
#7448=DIRECTION('',(-1.,0.,0.));
#7449=DIRECTION('',(0.,-6.53887346783621E-15,1.));
#7450=DIRECTION('',(-1.,0.,0.));
#7451=DIRECTION('',(0.,-6.53887346783621E-15,1.));
#7452=DIRECTION('',(-1.,0.,0.));
#7453=DIRECTION('',(0.,-6.53887346783621E-15,1.));
#7454=DIRECTION('',(-1.,0.,0.));
#7455=DIRECTION('',(0.,0.,1.));
#7456=DIRECTION('',(-1.,0.,0.));
#7457=DIRECTION('',(0.,-0.281732556841436,0.959492973614495));
#7458=DIRECTION('',(-1.,0.,0.));
#7459=DIRECTION('',(0.,-0.281732556841436,0.959492973614495));
#7460=DIRECTION('',(-1.,0.,0.));
#7461=DIRECTION('',(0.,-0.281732556841436,0.959492973614495));
#7462=DIRECTION('',(-1.,0.,0.));
#7463=DIRECTION('',(0.,0.,1.));
#7464=DIRECTION('',(-1.,0.,0.));
#7465=DIRECTION('',(0.,-0.540640817455604,0.841253532831177));
#7466=DIRECTION('',(-1.,0.,0.));
#7467=DIRECTION('',(0.,-0.540640817455604,0.841253532831177));
#7468=DIRECTION('',(-1.,0.,0.));
#7469=DIRECTION('',(0.,-0.540640817455604,0.841253532831177));
#7470=DIRECTION('',(-1.,0.,0.));
#7471=DIRECTION('',(0.,0.,1.));
#7472=DIRECTION('',(-1.,0.,0.));
#7473=DIRECTION('',(0.,-0.755749574354264,0.654860733945279));
#7474=DIRECTION('',(-1.,0.,0.));
#7475=DIRECTION('',(0.,-0.755749574354264,0.654860733945279));
#7476=DIRECTION('',(-1.,0.,0.));
#7477=DIRECTION('',(0.,-0.755749574354264,0.654860733945279));
#7478=DIRECTION('',(-1.,0.,0.));
#7479=DIRECTION('',(0.,0.,1.));
#7480=DIRECTION('',(-1.,0.,0.));
#7481=DIRECTION('',(0.,-0.909631995354522,0.415415013001878));
#7482=DIRECTION('',(-1.,0.,0.));
#7483=DIRECTION('',(0.,-0.909631995354522,0.415415013001878));
#7484=DIRECTION('',(-1.,0.,0.));
#7485=DIRECTION('',(0.,-0.909631995354522,0.415415013001878));
#7486=DIRECTION('',(-1.,0.,0.));
#7487=DIRECTION('',(0.,0.,1.));
#7488=DIRECTION('',(-1.,0.,0.));
#7489=DIRECTION('',(0.,-0.989821441880934,0.142314838273276));
#7490=DIRECTION('',(-1.,0.,0.));
#7491=DIRECTION('',(0.,-0.989821441880934,0.142314838273276));
#7492=DIRECTION('',(-1.,0.,0.));
#7493=DIRECTION('',(0.,-0.989821441880934,0.142314838273276));
#7494=DIRECTION('',(-1.,0.,0.));
#7495=DIRECTION('',(0.,0.,1.));
#7496=DIRECTION('',(-1.,0.,0.));
#7497=DIRECTION('',(0.,-0.989821441880931,-0.142314838273295));
#7498=DIRECTION('',(-1.,0.,0.));
#7499=DIRECTION('',(0.,-0.989821441880931,-0.142314838273295));
#7500=DIRECTION('',(-1.,0.,0.));
#7501=DIRECTION('',(0.,-0.989821441880931,-0.142314838273295));
#7502=DIRECTION('',(-1.,0.,0.));
#7503=DIRECTION('',(0.,0.,1.));
#7504=DIRECTION('',(-1.,0.,0.));
#7505=DIRECTION('',(0.,-0.909631995354514,-0.415415013001896));
#7506=DIRECTION('',(-1.,0.,0.));
#7507=DIRECTION('',(0.,-0.909631995354514,-0.415415013001896));
#7508=DIRECTION('',(-1.,0.,0.));
#7509=DIRECTION('',(0.,-0.909631995354514,-0.415415013001896));
#7510=DIRECTION('',(-1.,0.,0.));
#7511=DIRECTION('',(0.,0.,1.));
#7512=DIRECTION('',(-1.,0.,0.));
#7513=DIRECTION('',(0.,-0.755749574354251,-0.654860733945294));
#7514=DIRECTION('',(-1.,0.,0.));
#7515=DIRECTION('',(0.,-0.755749574354251,-0.654860733945294));
#7516=DIRECTION('',(-1.,0.,0.));
#7517=DIRECTION('',(0.,-0.755749574354251,-0.654860733945294));
#7518=DIRECTION('',(-1.,0.,0.));
#7519=DIRECTION('',(0.,0.,1.));
#7520=DIRECTION('',(-1.,0.,0.));
#7521=DIRECTION('',(0.,-0.540640817455587,-0.841253532831188));
#7522=DIRECTION('',(-1.,0.,0.));
#7523=DIRECTION('',(0.,-0.540640817455587,-0.841253532831188));
#7524=DIRECTION('',(-1.,0.,0.));
#7525=DIRECTION('',(0.,-0.540640817455587,-0.841253532831188));
#7526=DIRECTION('',(-1.,0.,0.));
#7527=DIRECTION('',(0.,0.,1.));
#7528=DIRECTION('',(-1.,0.,0.));
#7529=DIRECTION('',(0.,-0.281732556841418,-0.959492973614501));
#7530=DIRECTION('',(-1.,0.,0.));
#7531=DIRECTION('',(0.,-0.281732556841418,-0.959492973614501));
#7532=DIRECTION('',(-1.,0.,0.));
#7533=DIRECTION('',(0.,-0.281732556841418,-0.959492973614501));
#7534=DIRECTION('',(-1.,0.,0.));
#7535=DIRECTION('',(0.,0.,1.));
#7536=DIRECTION('',(-1.,0.,0.));
#7537=DIRECTION('',(0.,0.,-1.));
#7538=DIRECTION('',(-1.,0.,0.));
#7539=DIRECTION('',(0.,0.,-1.));
#7540=DIRECTION('',(-1.,0.,0.));
#7541=DIRECTION('',(0.,0.,-1.));
#7542=DIRECTION('',(-1.,0.,0.));
#7543=DIRECTION('',(0.,0.,1.));
#7544=DIRECTION('',(-1.,0.,0.));
#7545=DIRECTION('',(0.,0.281732556841431,-0.959492973614497));
#7546=DIRECTION('',(-1.,0.,0.));
#7547=DIRECTION('',(0.,0.281732556841431,-0.959492973614497));
#7548=DIRECTION('',(-1.,0.,0.));
#7549=DIRECTION('',(0.,0.281732556841431,-0.959492973614497));
#7550=DIRECTION('',(-1.,0.,0.));
#7551=DIRECTION('',(0.,0.,1.));
#7552=DIRECTION('',(-1.,0.,0.));
#7553=DIRECTION('',(0.,0.540640817455599,-0.84125353283118));
#7554=DIRECTION('',(-1.,0.,0.));
#7555=DIRECTION('',(0.,0.540640817455599,-0.84125353283118));
#7556=DIRECTION('',(-1.,0.,0.));
#7557=DIRECTION('',(0.,0.540640817455599,-0.84125353283118));
#7558=DIRECTION('',(-1.,0.,0.));
#7559=DIRECTION('',(0.,0.,1.));
#7560=DIRECTION('',(-1.,0.,0.));
#7561=DIRECTION('',(0.,0.75574957435426,-0.654860733945284));
#7562=DIRECTION('',(-1.,0.,0.));
#7563=DIRECTION('',(0.,0.75574957435426,-0.654860733945284));
#7564=DIRECTION('',(-1.,0.,0.));
#7565=DIRECTION('',(0.,0.75574957435426,-0.654860733945284));
#7566=DIRECTION('',(-1.,0.,0.));
#7567=DIRECTION('',(0.,0.,1.));
#7568=DIRECTION('',(-1.,0.,0.));
#7569=DIRECTION('',(0.,0.90963199535452,-0.415415013001884));
#7570=DIRECTION('',(-1.,0.,0.));
#7571=DIRECTION('',(0.,0.90963199535452,-0.415415013001884));
#7572=DIRECTION('',(-1.,0.,0.));
#7573=DIRECTION('',(0.,0.90963199535452,-0.415415013001884));
#7574=DIRECTION('',(-1.,0.,0.));
#7575=DIRECTION('',(0.,0.,1.));
#7576=DIRECTION('',(-1.,0.,0.));
#7577=DIRECTION('',(0.,0.989821441880933,-0.142314838273282));
#7578=DIRECTION('',(-1.,0.,0.));
#7579=DIRECTION('',(0.,0.989821441880933,-0.142314838273282));
#7580=DIRECTION('',(-1.,0.,0.));
#7581=DIRECTION('',(0.,0.989821441880933,-0.142314838273282));
#7582=DIRECTION('',(-1.,0.,0.));
#7583=DIRECTION('',(0.,0.,1.));
#7584=DIRECTION('',(-1.,0.,0.));
#7585=DIRECTION('',(0.,0.,1.));
#7586=DIRECTION('',(-1.,0.,0.));
#7587=DIRECTION('',(-1.,0.,0.));
#7588=DIRECTION('',(-1.,0.,0.));
#7589=DIRECTION('',(0.,0.,1.));
#7590=DIRECTION('',(-1.,0.,0.));
#7591=DIRECTION('',(0.,0.,1.));
#7592=DIRECTION('',(-1.,0.,0.));
#7593=DIRECTION('',(-1.,0.,0.));
#7594=DIRECTION('',(0.,0.,1.));
#7595=DIRECTION('',(-1.,0.,0.));
#7596=DIRECTION('',(-1.,0.,0.));
#7597=DIRECTION('',(0.,0.,1.));
#7598=DIRECTION('',(-1.,0.,0.));
#7599=DIRECTION('',(-1.,0.,0.));
#7600=DIRECTION('',(-1.,0.,0.));
#7601=DIRECTION('',(0.,0.,1.));
#7602=DIRECTION('',(-1.,0.,0.));
#7603=DIRECTION('',(0.,0.,1.));
#7604=DIRECTION('',(-1.,0.,0.));
#7605=DIRECTION('',(-1.,0.,0.));
#7606=DIRECTION('',(-1.,0.,0.));
#7607=DIRECTION('',(0.,0.,1.));
#7608=DIRECTION('',(-1.,0.,0.));
#7609=DIRECTION('',(0.,0.,1.));
#7610=DIRECTION('',(-1.,0.,0.));
#7611=DIRECTION('',(-1.,0.,0.));
#7612=DIRECTION('',(-1.,0.,0.));
#7613=DIRECTION('',(0.,0.,1.));
#7614=DIRECTION('',(-1.,0.,0.));
#7615=DIRECTION('',(0.,0.,1.));
#7616=DIRECTION('',(-1.,0.,0.));
#7617=DIRECTION('',(-1.,0.,0.));
#7618=DIRECTION('',(0.,0.,1.));
#7619=DIRECTION('',(-1.,0.,0.));
#7620=DIRECTION('',(-1.,0.,0.));
#7621=DIRECTION('',(0.,0.,1.));
#7622=DIRECTION('',(-1.,0.,0.));
#7623=DIRECTION('',(-1.,0.,0.));
#7624=DIRECTION('',(-1.,0.,0.));
#7625=DIRECTION('',(0.,0.,1.));
#7626=DIRECTION('',(-1.,0.,0.));
#7627=DIRECTION('',(0.,0.,1.));
#7628=DIRECTION('',(-1.,0.,0.));
#7629=DIRECTION('',(-1.,0.,0.));
#7630=DIRECTION('',(0.,0.,1.));
#7631=DIRECTION('',(-1.,0.,0.));
#7632=DIRECTION('',(-1.,0.,0.));
#7633=DIRECTION('',(0.,0.,1.));
#7634=DIRECTION('',(-1.,0.,0.));
#7635=DIRECTION('',(-1.,0.,0.));
#7636=DIRECTION('',(-1.,0.,0.));
#7637=DIRECTION('',(0.,0.,1.));
#7638=DIRECTION('',(-1.,0.,0.));
#7639=DIRECTION('',(0.,0.,1.));
#7640=DIRECTION('',(-1.,0.,0.));
#7641=DIRECTION('',(-1.,0.,0.));
#7642=DIRECTION('',(-1.,0.,0.));
#7643=DIRECTION('',(0.,0.,1.));
#7644=DIRECTION('',(-1.,0.,0.));
#7645=DIRECTION('',(0.,0.,1.));
#7646=DIRECTION('',(-1.,0.,0.));
#7647=DIRECTION('',(-1.,0.,0.));
#7648=DIRECTION('',(0.,0.,1.));
#7649=DIRECTION('',(-1.,0.,0.));
#7650=DIRECTION('',(-1.,0.,0.));
#7651=DIRECTION('',(0.,0.,1.));
#7652=DIRECTION('',(-1.,0.,0.));
#7653=DIRECTION('',(-1.,0.,0.));
#7654=DIRECTION('',(-1.,0.,0.));
#7655=DIRECTION('',(0.,0.,1.));
#7656=DIRECTION('',(-1.,0.,0.));
#7657=DIRECTION('',(0.,0.,1.));
#7658=DIRECTION('',(-1.,0.,0.));
#7659=DIRECTION('',(-1.,0.,0.));
#7660=DIRECTION('',(0.,0.,1.));
#7661=DIRECTION('',(-1.,0.,0.));
#7662=DIRECTION('',(-1.,0.,0.));
#7663=DIRECTION('',(0.,0.,1.));
#7664=DIRECTION('',(-1.,0.,0.));
#7665=DIRECTION('',(-1.,0.,0.));
#7666=DIRECTION('',(0.,0.,1.));
#7667=DIRECTION('',(-1.,0.,0.));
#7668=DIRECTION('',(-1.,0.,0.));
#7669=DIRECTION('',(0.,0.,1.));
#7670=DIRECTION('',(-1.,0.,0.));
#7671=DIRECTION('',(-1.,0.,0.));
#7672=DIRECTION('',(0.,0.,1.));
#7673=DIRECTION('',(-1.,0.,0.));
#7674=DIRECTION('',(-1.,0.,0.));
#7675=DIRECTION('',(0.,0.,1.));
#7676=DIRECTION('',(-1.,0.,0.));
#7677=DIRECTION('',(-1.,0.,0.));
#7678=DIRECTION('',(-1.,0.,0.));
#7679=DIRECTION('',(0.,0.,1.));
#7680=DIRECTION('',(-1.,0.,0.));
#7681=DIRECTION('',(0.,0.,1.));
#7682=DIRECTION('',(-1.,0.,0.));
#7683=DIRECTION('',(-1.,0.,0.));
#7684=DIRECTION('',(-1.,0.,0.));
#7685=DIRECTION('',(0.,0.,1.));
#7686=DIRECTION('',(-1.,0.,0.));
#7687=DIRECTION('',(0.,0.,1.));
#7688=DIRECTION('',(-1.,0.,0.));
#7689=DIRECTION('',(-1.,0.,0.));
#7690=DIRECTION('',(0.,0.,1.));
#7691=DIRECTION('',(-1.,0.,0.));
#7692=DIRECTION('',(-1.,0.,0.));
#7693=DIRECTION('',(0.,0.,1.));
#7694=DIRECTION('',(-1.,0.,0.));
#7695=DIRECTION('',(-1.,0.,0.));
#7696=DIRECTION('',(0.,0.,1.));
#7697=DIRECTION('',(-1.,0.,0.));
#7698=DIRECTION('',(-1.,0.,0.));
#7699=DIRECTION('',(0.,0.,1.));
#7700=DIRECTION('',(-1.,0.,0.));
#7701=DIRECTION('',(-1.,0.,0.));
#7702=DIRECTION('',(0.,0.,1.));
#7703=DIRECTION('',(-1.,0.,0.));
#7704=DIRECTION('',(-1.,0.,0.));
#7705=DIRECTION('',(0.,0.,1.));
#7706=DIRECTION('',(-1.,0.,0.));
#7707=DIRECTION('',(-1.,0.,0.));
#7708=DIRECTION('',(-1.,0.,0.));
#7709=DIRECTION('',(0.,0.,1.));
#7710=DIRECTION('',(1.,0.,0.));
#7711=DIRECTION('',(0.,0.,-1.));
#7712=DIRECTION('',(-1.,0.,0.));
#7713=DIRECTION('',(0.,0.989821441880932,0.142314838273289));
#7714=DIRECTION('',(1.,0.,0.));
#7715=DIRECTION('',(0.,0.,-1.));
#7716=DIRECTION('',(-1.,0.,0.));
#7717=DIRECTION('',(0.,0.989821441880933,-0.142314838273282));
#7718=DIRECTION('',(-1.,0.,0.));
#7719=DIRECTION('',(0.,0.989821441880933,-0.142314838273282));
#7720=DIRECTION('',(1.,0.,0.));
#7721=DIRECTION('',(0.,0.,-1.));
#7722=DIRECTION('',(-1.,0.,0.));
#7723=DIRECTION('',(0.,0.90963199535452,-0.415415013001884));
#7724=DIRECTION('',(-1.,0.,0.));
#7725=DIRECTION('',(0.,0.90963199535452,-0.415415013001884));
#7726=DIRECTION('',(1.,0.,0.));
#7727=DIRECTION('',(0.,0.,-1.));
#7728=DIRECTION('',(-1.,0.,0.));
#7729=DIRECTION('',(0.,0.75574957435426,-0.654860733945284));
#7730=DIRECTION('',(-1.,0.,0.));
#7731=DIRECTION('',(0.,0.75574957435426,-0.654860733945284));
#7732=DIRECTION('',(1.,0.,0.));
#7733=DIRECTION('',(0.,0.,-1.));
#7734=DIRECTION('',(-1.,0.,0.));
#7735=DIRECTION('',(0.,0.540640817455599,-0.84125353283118));
#7736=DIRECTION('',(-1.,0.,0.));
#7737=DIRECTION('',(0.,0.540640817455599,-0.84125353283118));
#7738=DIRECTION('',(1.,0.,0.));
#7739=DIRECTION('',(0.,0.,-1.));
#7740=DIRECTION('',(-1.,0.,0.));
#7741=DIRECTION('',(0.,0.281732556841431,-0.959492973614497));
#7742=DIRECTION('',(-1.,0.,0.));
#7743=DIRECTION('',(0.,0.281732556841431,-0.959492973614497));
#7744=DIRECTION('',(-1.,0.,0.));
#7745=DIRECTION('',(0.,0.,1.));
#7746=DIRECTION('',(1.,0.,0.));
#7747=DIRECTION('',(0.,0.,-1.));
#7748=DIRECTION('',(-1.,0.,0.));
#7749=DIRECTION('',(0.,0.,-1.));
#7750=DIRECTION('',(-1.,0.,0.));
#7751=DIRECTION('',(0.,0.,-1.));
#7752=DIRECTION('',(1.,0.,0.));
#7753=DIRECTION('',(0.,0.,-1.));
#7754=DIRECTION('',(-1.,0.,0.));
#7755=DIRECTION('',(0.,-0.281732556841418,-0.959492973614501));
#7756=DIRECTION('',(-1.,0.,0.));
#7757=DIRECTION('',(0.,-0.281732556841418,-0.959492973614501));
#7758=DIRECTION('',(1.,0.,0.));
#7759=DIRECTION('',(0.,0.,-1.));
#7760=DIRECTION('',(-1.,0.,0.));
#7761=DIRECTION('',(0.,-0.540640817455587,-0.841253532831188));
#7762=DIRECTION('',(-1.,0.,0.));
#7763=DIRECTION('',(0.,-0.540640817455587,-0.841253532831188));
#7764=DIRECTION('',(1.,0.,0.));
#7765=DIRECTION('',(0.,0.,-1.));
#7766=DIRECTION('',(-1.,0.,0.));
#7767=DIRECTION('',(0.,-0.755749574354251,-0.654860733945294));
#7768=DIRECTION('',(-1.,0.,0.));
#7769=DIRECTION('',(0.,-0.755749574354251,-0.654860733945294));
#7770=DIRECTION('',(1.,0.,0.));
#7771=DIRECTION('',(0.,0.,-1.));
#7772=DIRECTION('',(-1.,0.,0.));
#7773=DIRECTION('',(0.,-0.909631995354514,-0.415415013001896));
#7774=DIRECTION('',(-1.,0.,0.));
#7775=DIRECTION('',(0.,-0.909631995354514,-0.415415013001896));
#7776=DIRECTION('',(1.,0.,0.));
#7777=DIRECTION('',(0.,0.,-1.));
#7778=DIRECTION('',(-1.,0.,0.));
#7779=DIRECTION('',(0.,-0.989821441880931,-0.142314838273295));
#7780=DIRECTION('',(-1.,0.,0.));
#7781=DIRECTION('',(0.,-0.989821441880931,-0.142314838273295));
#7782=DIRECTION('',(1.,0.,0.));
#7783=DIRECTION('',(0.,0.,-1.));
#7784=DIRECTION('',(-1.,0.,0.));
#7785=DIRECTION('',(0.,-0.989821441880934,0.142314838273276));
#7786=DIRECTION('',(-1.,0.,0.));
#7787=DIRECTION('',(0.,-0.989821441880934,0.142314838273276));
#7788=DIRECTION('',(1.,0.,0.));
#7789=DIRECTION('',(0.,0.,-1.));
#7790=DIRECTION('',(-1.,0.,0.));
#7791=DIRECTION('',(0.,-0.909631995354522,0.415415013001878));
#7792=DIRECTION('',(-1.,0.,0.));
#7793=DIRECTION('',(0.,-0.909631995354522,0.415415013001878));
#7794=DIRECTION('',(1.,0.,0.));
#7795=DIRECTION('',(0.,0.,-1.));
#7796=DIRECTION('',(-1.,0.,0.));
#7797=DIRECTION('',(0.,-0.755749574354264,0.654860733945279));
#7798=DIRECTION('',(-1.,0.,0.));
#7799=DIRECTION('',(0.,-0.755749574354264,0.654860733945279));
#7800=DIRECTION('',(1.,0.,0.));
#7801=DIRECTION('',(0.,0.,-1.));
#7802=DIRECTION('',(-1.,0.,0.));
#7803=DIRECTION('',(0.,-0.540640817455604,0.841253532831177));
#7804=DIRECTION('',(-1.,0.,0.));
#7805=DIRECTION('',(0.,-0.540640817455604,0.841253532831177));
#7806=DIRECTION('',(1.,0.,0.));
#7807=DIRECTION('',(0.,0.,-1.));
#7808=DIRECTION('',(-1.,0.,0.));
#7809=DIRECTION('',(0.,-0.281732556841436,0.959492973614495));
#7810=DIRECTION('',(-1.,0.,0.));
#7811=DIRECTION('',(0.,-0.281732556841436,0.959492973614495));
#7812=DIRECTION('',(1.,0.,0.));
#7813=DIRECTION('',(0.,0.,-1.));
#7814=DIRECTION('',(-1.,0.,0.));
#7815=DIRECTION('',(0.,-6.53887346783621E-15,1.));
#7816=DIRECTION('',(-1.,0.,0.));
#7817=DIRECTION('',(0.,-6.53887346783621E-15,1.));
#7818=DIRECTION('',(1.,0.,0.));
#7819=DIRECTION('',(0.,0.,-1.));
#7820=DIRECTION('',(-1.,0.,0.));
#7821=DIRECTION('',(0.,0.281732556841424,0.959492973614499));
#7822=DIRECTION('',(-1.,0.,0.));
#7823=DIRECTION('',(0.,0.281732556841424,0.959492973614499));
#7824=DIRECTION('',(1.,0.,0.));
#7825=DIRECTION('',(0.,0.,-1.));
#7826=DIRECTION('',(-1.,0.,0.));
#7827=DIRECTION('',(0.,0.540640817455593,0.841253532831184));
#7828=DIRECTION('',(-1.,0.,0.));
#7829=DIRECTION('',(0.,0.540640817455593,0.841253532831184));
#7830=DIRECTION('',(1.,0.,0.));
#7831=DIRECTION('',(0.,0.,-1.));
#7832=DIRECTION('',(-1.,0.,0.));
#7833=DIRECTION('',(0.,0.755749574354255,0.654860733945289));
#7834=DIRECTION('',(-1.,0.,0.));
#7835=DIRECTION('',(0.,0.755749574354255,0.654860733945289));
#7836=DIRECTION('',(1.,0.,0.));
#7837=DIRECTION('',(0.,0.,-1.));
#7838=DIRECTION('',(-1.,0.,0.));
#7839=DIRECTION('',(0.,0.909631995354517,0.41541501300189));
#7840=DIRECTION('',(-1.,0.,0.));
#7841=DIRECTION('',(0.,0.909631995354517,0.41541501300189));
#7842=DIRECTION('',(1.,0.,0.));
#7843=DIRECTION('',(0.,0.,-1.));
#7844=DIRECTION('',(-1.,0.,0.));
#7845=DIRECTION('',(0.,0.989821441880932,0.142314838273289));
#7846=DIRECTION('',(-1.,0.,0.));
#7847=DIRECTION('',(0.,0.,1.));
#7848=DIRECTION('',(-1.,0.,0.));
#7849=DIRECTION('',(-1.,0.,0.));
#7850=DIRECTION('',(-1.,0.,0.));
#7851=DIRECTION('',(0.,0.,1.));
#7852=DIRECTION('',(-1.,0.,0.));
#7853=DIRECTION('',(-1.,0.,0.));
#7854=DIRECTION('',(0.,0.,1.));
#7855=DIRECTION('',(-1.,0.,0.));
#7856=DIRECTION('',(-1.,0.,0.));
#7857=DIRECTION('',(0.,0.,1.));
#7858=DIRECTION('',(-1.,0.,0.));
#7859=DIRECTION('',(0.,0.,1.));
#7860=DIRECTION('',(-1.,0.,0.));
#7861=DIRECTION('',(-1.,0.,0.));
#7862=DIRECTION('',(0.,0.,1.));
#7863=DIRECTION('',(-1.,0.,0.));
#7864=DIRECTION('',(-1.,0.,0.));
#7865=DIRECTION('',(0.,0.,1.));
#7866=DIRECTION('',(-1.,0.,0.));
#7867=DIRECTION('',(0.,0.,1.));
#7868=DIRECTION('',(-1.,0.,0.));
#7869=DIRECTION('',(-1.,0.,0.));
#7870=DIRECTION('',(0.,0.,1.));
#7871=DIRECTION('',(-1.,0.,0.));
#7872=DIRECTION('',(-1.,0.,0.));
#7873=DIRECTION('',(0.,0.,1.));
#7874=DIRECTION('',(-1.,0.,0.));
#7875=DIRECTION('',(0.,0.,1.));
#7876=DIRECTION('',(-1.,0.,0.));
#7877=DIRECTION('',(-1.,0.,0.));
#7878=DIRECTION('',(0.,0.,1.));
#7879=DIRECTION('',(-1.,0.,0.));
#7880=DIRECTION('',(-1.,0.,0.));
#7881=DIRECTION('',(0.,0.,1.));
#7882=DIRECTION('',(-1.,0.,0.));
#7883=DIRECTION('',(0.,0.,1.));
#7884=DIRECTION('',(-1.,0.,0.));
#7885=DIRECTION('',(-1.,0.,0.));
#7886=DIRECTION('',(0.,0.,1.));
#7887=DIRECTION('',(-1.,0.,0.));
#7888=DIRECTION('',(-1.,0.,0.));
#7889=DIRECTION('',(0.,0.,1.));
#7890=DIRECTION('',(-1.,0.,0.));
#7891=DIRECTION('',(0.,0.,1.));
#7892=DIRECTION('',(-1.,0.,0.));
#7893=DIRECTION('',(-1.,0.,0.));
#7894=DIRECTION('',(0.,0.,1.));
#7895=DIRECTION('',(-1.,0.,0.));
#7896=DIRECTION('',(-1.,0.,0.));
#7897=DIRECTION('',(0.,0.,1.));
#7898=DIRECTION('',(-1.,0.,0.));
#7899=DIRECTION('',(0.,0.,1.));
#7900=DIRECTION('',(-1.,0.,0.));
#7901=DIRECTION('',(-1.,0.,0.));
#7902=DIRECTION('',(0.,0.,1.));
#7903=DIRECTION('',(-1.,0.,0.));
#7904=DIRECTION('',(-1.,0.,0.));
#7905=DIRECTION('',(0.,0.,1.));
#7906=DIRECTION('',(-1.,0.,0.));
#7907=DIRECTION('',(0.,0.,1.));
#7908=DIRECTION('',(-1.,0.,0.));
#7909=DIRECTION('',(-1.,0.,0.));
#7910=DIRECTION('',(0.,0.,1.));
#7911=DIRECTION('',(-1.,0.,0.));
#7912=DIRECTION('',(-1.,0.,0.));
#7913=DIRECTION('',(0.,0.,1.));
#7914=DIRECTION('',(-1.,0.,0.));
#7915=DIRECTION('',(0.,0.,1.));
#7916=DIRECTION('',(-1.,0.,0.));
#7917=DIRECTION('',(-1.,0.,0.));
#7918=DIRECTION('',(0.,0.,1.));
#7919=DIRECTION('',(-1.,0.,0.));
#7920=DIRECTION('',(-1.,0.,0.));
#7921=DIRECTION('',(0.,0.,1.));
#7922=DIRECTION('',(-1.,0.,0.));
#7923=DIRECTION('',(0.,0.,1.));
#7924=DIRECTION('',(-1.,0.,0.));
#7925=DIRECTION('',(-1.,0.,0.));
#7926=DIRECTION('',(0.,0.,1.));
#7927=DIRECTION('',(-1.,0.,0.));
#7928=DIRECTION('',(-1.,0.,0.));
#7929=DIRECTION('',(0.,0.,1.));
#7930=DIRECTION('',(-1.,0.,0.));
#7931=DIRECTION('',(0.,0.,1.));
#7932=DIRECTION('',(-1.,0.,0.));
#7933=DIRECTION('',(-1.,0.,0.));
#7934=DIRECTION('',(0.,0.,1.));
#7935=DIRECTION('',(-1.,0.,0.));
#7936=DIRECTION('',(-1.,0.,0.));
#7937=DIRECTION('',(0.,0.,1.));
#7938=DIRECTION('',(-1.,0.,0.));
#7939=DIRECTION('',(0.,0.,1.));
#7940=DIRECTION('',(-1.,0.,0.));
#7941=DIRECTION('',(-1.,0.,0.));
#7942=DIRECTION('',(0.,0.,1.));
#7943=DIRECTION('',(-1.,0.,0.));
#7944=DIRECTION('',(-1.,0.,0.));
#7945=DIRECTION('',(0.,0.,1.));
#7946=DIRECTION('',(-1.,0.,0.));
#7947=DIRECTION('',(0.,0.,1.));
#7948=DIRECTION('',(-1.,0.,0.));
#7949=DIRECTION('',(-1.,0.,0.));
#7950=DIRECTION('',(0.,0.,1.));
#7951=DIRECTION('',(-1.,0.,0.));
#7952=DIRECTION('',(-1.,0.,0.));
#7953=DIRECTION('',(0.,0.,1.));
#7954=DIRECTION('',(-1.,0.,0.));
#7955=DIRECTION('',(0.,0.,1.));
#7956=DIRECTION('',(-1.,0.,0.));
#7957=DIRECTION('',(-1.,0.,0.));
#7958=DIRECTION('',(0.,0.,1.));
#7959=DIRECTION('',(-1.,0.,0.));
#7960=DIRECTION('',(-1.,0.,0.));
#7961=DIRECTION('',(0.,0.,1.));
#7962=DIRECTION('',(-1.,0.,0.));
#7963=DIRECTION('',(0.,0.,1.));
#7964=DIRECTION('',(-1.,0.,0.));
#7965=DIRECTION('',(-1.,0.,0.));
#7966=DIRECTION('',(0.,0.,1.));
#7967=DIRECTION('',(-1.,0.,0.));
#7968=DIRECTION('',(-1.,0.,0.));
#7969=DIRECTION('',(0.,0.,1.));
#7970=DIRECTION('',(-1.,0.,0.));
#7971=DIRECTION('',(0.,0.,1.));
#7972=DIRECTION('',(-1.,0.,0.));
#7973=DIRECTION('',(-1.,0.,0.));
#7974=DIRECTION('',(0.,0.,1.));
#7975=DIRECTION('',(-1.,0.,0.));
#7976=DIRECTION('',(-1.,0.,0.));
#7977=DIRECTION('',(0.,0.,1.));
#7978=DIRECTION('',(-1.,0.,0.));
#7979=DIRECTION('',(0.,0.,1.));
#7980=DIRECTION('',(-1.,0.,0.));
#7981=DIRECTION('',(-1.,0.,0.));
#7982=DIRECTION('',(0.,0.,1.));
#7983=DIRECTION('',(-1.,0.,0.));
#7984=DIRECTION('',(-1.,0.,0.));
#7985=DIRECTION('',(0.,0.,1.));
#7986=DIRECTION('',(-1.,0.,0.));
#7987=DIRECTION('',(0.,0.,1.));
#7988=DIRECTION('',(-1.,0.,0.));
#7989=DIRECTION('',(-1.,0.,0.));
#7990=DIRECTION('',(0.,0.,1.));
#7991=DIRECTION('',(-1.,0.,0.));
#7992=DIRECTION('',(-1.,0.,0.));
#7993=DIRECTION('',(0.,0.,1.));
#7994=DIRECTION('',(-1.,0.,0.));
#7995=DIRECTION('',(0.,0.,1.));
#7996=DIRECTION('',(-1.,0.,0.));
#7997=DIRECTION('',(-1.,0.,0.));
#7998=DIRECTION('',(0.,0.,1.));
#7999=DIRECTION('',(-1.,0.,0.));
#8000=DIRECTION('',(-1.,0.,0.));
#8001=DIRECTION('',(0.,0.,1.));
#8002=DIRECTION('',(-1.,0.,0.));
#8003=DIRECTION('',(0.,0.,1.));
#8004=DIRECTION('',(-1.,0.,0.));
#8005=DIRECTION('',(-1.,0.,0.));
#8006=DIRECTION('',(0.,0.,1.));
#8007=DIRECTION('',(-1.,0.,0.));
#8008=DIRECTION('',(-1.,0.,0.));
#8009=DIRECTION('',(0.,0.,1.));
#8010=DIRECTION('',(-1.,0.,0.));
#8011=DIRECTION('',(0.,0.,1.));
#8012=DIRECTION('',(-1.,0.,0.));
#8013=DIRECTION('',(-1.,0.,0.));
#8014=DIRECTION('',(0.,0.,1.));
#8015=DIRECTION('',(-1.,0.,0.));
#8016=DIRECTION('',(-1.,0.,0.));
#8017=DIRECTION('',(0.,0.,1.));
#8018=DIRECTION('',(-1.,0.,0.));
#8019=DIRECTION('',(0.,0.,1.));
#8020=DIRECTION('',(-1.,0.,0.));
#8021=DIRECTION('',(-1.,0.,0.));
#8022=DIRECTION('',(0.,0.,1.));
#8023=DIRECTION('',(-1.,0.,0.));
#8024=DIRECTION('',(-1.,0.,0.));
#8025=DIRECTION('',(0.,0.,1.));
#8026=DIRECTION('',(1.,0.,0.));
#8027=DIRECTION('',(0.,0.,-1.));
#8028=DIRECTION('',(1.,0.,0.));
#8029=DIRECTION('',(0.,0.,-1.));
#8030=DIRECTION('',(1.,0.,0.));
#8031=DIRECTION('',(0.,0.,-1.));
#8032=DIRECTION('',(1.,0.,0.));
#8033=DIRECTION('',(0.,0.,-1.));
#8034=DIRECTION('',(1.,0.,0.));
#8035=DIRECTION('',(0.,0.,-1.));
#8036=DIRECTION('',(1.,0.,0.));
#8037=DIRECTION('',(0.,0.,-1.));
#8038=DIRECTION('',(1.,0.,0.));
#8039=DIRECTION('',(0.,0.,-1.));
#8040=DIRECTION('',(-1.,0.,0.));
#8041=DIRECTION('',(0.,0.,1.));
#8042=DIRECTION('',(1.,0.,0.));
#8043=DIRECTION('',(0.,0.,-1.));
#8044=DIRECTION('',(1.,0.,0.));
#8045=DIRECTION('',(0.,0.,-1.));
#8046=DIRECTION('',(1.,0.,0.));
#8047=DIRECTION('',(0.,0.,-1.));
#8048=DIRECTION('',(1.,0.,0.));
#8049=DIRECTION('',(0.,0.,-1.));
#8050=DIRECTION('',(-1.,0.,0.));
#8051=DIRECTION('',(0.,0.,1.));
#8052=DIRECTION('',(1.,0.,0.));
#8053=DIRECTION('',(0.,0.,-1.));
#8391=CARTESIAN_POINT('',(0.,0.,0.));
#9234=CARTESIAN_POINT('',(0.0500000508,0.,0.));
#9235=CARTESIAN_POINT('',(0.,0.,0.));
#9236=CARTESIAN_POINT('',(0.,0.,-0.0015));
#9237=CARTESIAN_POINT('',(0.01,0.,0.));
#9238=CARTESIAN_POINT('',(0.01,0.,-0.0015));
#9239=CARTESIAN_POINT('',(0.015,0.,0.));
#9240=CARTESIAN_POINT('',(0.005,0.,0.));
#9241=CARTESIAN_POINT('',(0.005,0.,0.0025));
#9242=CARTESIAN_POINT('',(0.01,0.,0.));
#9243=CARTESIAN_POINT('',(0.01,0.,-0.0025));
#9244=CARTESIAN_POINT('',(0.005,0.,0.));
#9245=CARTESIAN_POINT('',(0.005,0.00175014931247276,0.00486296201856249));
#9246=CARTESIAN_POINT('',(0.005,-0.000449829019689083,0.00485319789963747));
#9247=CARTESIAN_POINT('',(0.005,-0.000134141743660394,0.00599850031196196));
#9248=CARTESIAN_POINT('',(0.005,0.,0.));
#9249=CARTESIAN_POINT('',(0.005,-0.000935696069402783,0.00478334076412126));
#9250=CARTESIAN_POINT('',(0.005,-0.00304931069140626,0.00417290384710763));
#9251=CARTESIAN_POINT('',(0.005,-0.00156126476959266,0.00579331099797247));
#9252=CARTESIAN_POINT('',(0.005,0.,0.));
#9253=CARTESIAN_POINT('',(0.005,-0.0018186808906137,0.00571772680513126));
#9254=CARTESIAN_POINT('',(0.005,0.000309201244781488,0.0051590519284221));
#9255=CARTESIAN_POINT('',(0.005,-0.0017989116368419,0.00452987780440431));
#9256=CARTESIAN_POINT('',(0.005,0.,0.));
#9257=CARTESIAN_POINT('',(0.005,-0.0022454166277504,0.00432596580751883));
#9258=CARTESIAN_POINT('',(0.005,-0.00410143505307095,0.00314478182317488));
#9259=CARTESIAN_POINT('',(0.005,-0.00313018689641237,0.00511878208107439));
#9260=CARTESIAN_POINT('',(0.005,0.,0.));
#9261=CARTESIAN_POINT('',(0.005,-0.00335588132792122,0.00497373707717946));
#9262=CARTESIAN_POINT('',(0.005,-0.00115679646887138,0.00503718613310417));
#9263=CARTESIAN_POINT('',(0.005,-0.00300225713171722,0.00383957394967893));
#9264=CARTESIAN_POINT('',(0.005,0.,0.));
#9265=CARTESIAN_POINT('',(0.005,-0.00337322688492455,0.0035181268287005));
#9266=CARTESIAN_POINT('',(0.005,-0.00482128553890929,0.00186188827866615));
#9267=CARTESIAN_POINT('',(0.005,-0.00444551989682302,0.00402955988253688));
#9268=CARTESIAN_POINT('',(0.005,0.,0.));
#9269=CARTESIAN_POINT('',(0.005,-0.00462120821823529,0.00382680475118794));
#9270=CARTESIAN_POINT('',(0.005,-0.00252907741234978,0.00450723747458156));
#9271=CARTESIAN_POINT('',(0.005,-0.00396237760889148,0.00283821064837608));
#9272=CARTESIAN_POINT('',(0.005,0.,0.));
#9273=CARTESIAN_POINT('',(0.005,-0.00422775836123484,0.00242527013732674));
#9274=CARTESIAN_POINT('',(0.005,-0.00515054414367435,0.000428155618895829));
#9275=CARTESIAN_POINT('',(0.005,-0.0054007033137179,0.00261388670703158));
#9276=CARTESIAN_POINT('',(0.005,0.,0.));
#9277=CARTESIAN_POINT('',(0.005,-0.00551215230209144,0.00236984746313935));
#9278=CARTESIAN_POINT('',(0.005,-0.00369646754488213,0.00361213924144174));
#9279=CARTESIAN_POINT('',(0.005,-0.00460148981736036,0.00160691239983047));
#9280=CARTESIAN_POINT('',(0.005,0.,0.));
#9281=CARTESIAN_POINT('',(0.005,-0.004739781998565,0.00113593248306364));
#9282=CARTESIAN_POINT('',(0.005,-0.00506253629338438,-0.00104026366277791));
#9283=CARTESIAN_POINT('',(0.005,-0.0059183538673547,0.000986451975905413));
#9284=CARTESIAN_POINT('',(0.005,0.,0.));
#9285=CARTESIAN_POINT('',(0.005,-0.00595653458846414,0.000720899227652746));
#9286=CARTESIAN_POINT('',(0.005,-0.00456439186066708,0.00242440696917955));
#9287=CARTESIAN_POINT('',(0.005,-0.00486781668694036,0.000245431665326605));
#9288=CARTESIAN_POINT('',(0.005,0.,0.));
#9289=CARTESIAN_POINT('',(0.005,-0.00486781668694036,-0.000245431665326668));
#9290=CARTESIAN_POINT('',(0.005,-0.00456439186066704,-0.00242440696917961));
#9291=CARTESIAN_POINT('',(0.005,-0.00595653458846413,-0.000720899227652823));
#9292=CARTESIAN_POINT('',(0.005,0.,0.));
#9293=CARTESIAN_POINT('',(0.005,-0.00591835386735468,-0.000986451975905493));
#9294=CARTESIAN_POINT('',(0.005,-0.0050625362933844,0.00104026366277785));
#9295=CARTESIAN_POINT('',(0.005,-0.00473978199856499,-0.00113593248306371));
#9296=CARTESIAN_POINT('',(0.005,0.,0.));
#9297=CARTESIAN_POINT('',(0.005,-0.00460148981736034,-0.00160691239983053));
#9298=CARTESIAN_POINT('',(0.005,-0.00369646754488208,-0.00361213924144179));
#9299=CARTESIAN_POINT('',(0.005,-0.00551215230209141,-0.00236984746313942));
#9300=CARTESIAN_POINT('',(0.005,0.,0.));
#9301=CARTESIAN_POINT('',(0.005,-0.00540070331371787,-0.00261388670703166));
#9302=CARTESIAN_POINT('',(0.005,-0.00515054414367434,-0.0004281556188959));
#9303=CARTESIAN_POINT('',(0.005,-0.00422775836123482,-0.0024252701373268));
#9304=CARTESIAN_POINT('',(0.005,0.,0.));
#9305=CARTESIAN_POINT('',(0.005,-0.00396237760889144,-0.00283821064837614));
#9306=CARTESIAN_POINT('',(0.005,-0.00252907741234972,-0.00450723747458159));
#9307=CARTESIAN_POINT('',(0.005,-0.00462120821823524,-0.003826804751188));
#9308=CARTESIAN_POINT('',(0.005,0.,0.));
#9309=CARTESIAN_POINT('',(0.005,-0.00444551989682297,-0.00402955988253693));
#9310=CARTESIAN_POINT('',(0.005,-0.00482128553890927,-0.00186188827866621));
#9311=CARTESIAN_POINT('',(0.005,-0.0033732268849245,-0.00351812682870055));
#9312=CARTESIAN_POINT('',(0.005,0.,0.));
#9313=CARTESIAN_POINT('',(0.005,-0.00300225713171717,-0.00383957394967897));
#9314=CARTESIAN_POINT('',(0.005,-0.00115679646887131,-0.00503718613310418));
#9315=CARTESIAN_POINT('',(0.005,-0.00335588132792115,-0.00497373707717951));
#9316=CARTESIAN_POINT('',(0.005,0.,0.));
#9317=CARTESIAN_POINT('',(0.005,-0.0031301868964123,-0.00511878208107443));
#9318=CARTESIAN_POINT('',(0.005,-0.0041014350530709,-0.00314478182317494));
#9319=CARTESIAN_POINT('',(0.005,-0.00224541662775034,-0.00432596580751886));
#9320=CARTESIAN_POINT('',(0.005,0.,0.));
#9321=CARTESIAN_POINT('',(0.005,-0.00179891163684184,-0.00452987780440433));
#9322=CARTESIAN_POINT('',(0.005,0.000309201244781555,-0.0051590519284221));
#9323=CARTESIAN_POINT('',(0.005,-0.00181868089061363,-0.00571772680513128));
#9324=CARTESIAN_POINT('',(0.005,0.,0.));
#9325=CARTESIAN_POINT('',(0.005,-0.00156126476959258,-0.00579331099797249));
#9326=CARTESIAN_POINT('',(0.005,-0.0030493106914062,-0.00417290384710767));
#9327=CARTESIAN_POINT('',(0.005,-0.000935696069402719,-0.00478334076412128));
#9328=CARTESIAN_POINT('',(0.005,0.,0.));
#9329=CARTESIAN_POINT('',(0.005,-0.000449829019689018,-0.00485319789963748));
#9330=CARTESIAN_POINT('',(0.005,0.00175014931247283,-0.00486296201856246));
#9331=CARTESIAN_POINT('',(0.005,-0.000134141743660314,-0.00599850031196196));
#9332=CARTESIAN_POINT('',(0.005,0.,0.));
#9333=CARTESIAN_POINT('',(0.005,0.000134141743660434,-0.00599850031196196));
#9334=CARTESIAN_POINT('',(0.005,-0.00175014931247273,-0.0048629620185625));
#9335=CARTESIAN_POINT('',(0.005,0.000449829019689116,-0.00485319789963747));
#9336=CARTESIAN_POINT('',(0.005,0.,0.));
#9337=CARTESIAN_POINT('',(0.005,0.000935696069402815,-0.00478334076412126));
#9338=CARTESIAN_POINT('',(0.005,0.00304931069140629,-0.00417290384710761));
#9339=CARTESIAN_POINT('',(0.005,0.00156126476959269,-0.00579331099797246));
#9340=CARTESIAN_POINT('',(0.005,0.,0.));
#9341=CARTESIAN_POINT('',(0.005,0.00181868089061374,-0.00571772680513125));
#9342=CARTESIAN_POINT('',(0.005,-0.000309201244781452,-0.0051590519284221));
#9343=CARTESIAN_POINT('',(0.005,0.00179891163684193,-0.0045298778044043));
#9344=CARTESIAN_POINT('',(0.005,0.,0.));
#9345=CARTESIAN_POINT('',(0.005,0.00224541662775043,-0.00432596580751882));
#9346=CARTESIAN_POINT('',(0.005,0.00410143505307097,-0.00314478182317485));
#9347=CARTESIAN_POINT('',(0.005,0.0031301868964124,-0.00511878208107437));
#9348=CARTESIAN_POINT('',(0.005,0.,0.));
#9349=CARTESIAN_POINT('',(0.005,0.00335588132792125,-0.00497373707717944));
#9350=CARTESIAN_POINT('',(0.005,0.00115679646887141,-0.00503718613310416));
#9351=CARTESIAN_POINT('',(0.005,0.00300225713171725,-0.00383957394967891));
#9352=CARTESIAN_POINT('',(0.005,0.,0.));
#9353=CARTESIAN_POINT('',(0.005,0.00337322688492458,-0.00351812682870047));
#9354=CARTESIAN_POINT('',(0.005,0.0048212855389093,-0.00186188827866611));
#9355=CARTESIAN_POINT('',(0.005,0.00444551989682306,-0.00402955988253685));
#9356=CARTESIAN_POINT('',(0.005,0.,0.));
#9357=CARTESIAN_POINT('',(0.005,0.00462120821823532,-0.00382680475118791));
#9358=CARTESIAN_POINT('',(0.005,0.00252907741234981,-0.00450723747458154));
#9359=CARTESIAN_POINT('',(0.005,0.0039623776088915,-0.00283821064837605));
#9360=CARTESIAN_POINT('',(0.005,0.,0.));
#9361=CARTESIAN_POINT('',(0.005,0.00422775836123486,-0.00242527013732671));
#9362=CARTESIAN_POINT('',(0.005,0.00515054414367435,-0.000428155618895793));
#9363=CARTESIAN_POINT('',(0.005,0.00540070331371792,-0.00261388670703155));
#9364=CARTESIAN_POINT('',(0.005,0.,0.));
#9365=CARTESIAN_POINT('',(0.005,0.00551215230209146,-0.00236984746313931));
#9366=CARTESIAN_POINT('',(0.005,0.00369646754488215,-0.00361213924144172));
#9367=CARTESIAN_POINT('',(0.005,0.00460148981736037,-0.00160691239983044));
#9368=CARTESIAN_POINT('',(0.005,0.,0.));
#9369=CARTESIAN_POINT('',(0.005,0.00473978199856501,-0.00113593248306361));
#9370=CARTESIAN_POINT('',(0.005,0.00506253629338438,0.00104026366277795));
#9371=CARTESIAN_POINT('',(0.005,0.0059183538673547,-0.000986451975905376));
#9372=CARTESIAN_POINT('',(0.005,0.,0.));
#9373=CARTESIAN_POINT('',(0.005,0.00595653458846413,-0.000720899227652784));
#9374=CARTESIAN_POINT('',(0.005,0.00456439186066706,-0.00242440696917958));
#9375=CARTESIAN_POINT('',(0.005,0.00486781668694036,-0.000245431665326637));
#9376=CARTESIAN_POINT('',(0.005,0.,0.));
#9377=CARTESIAN_POINT('',(0.005,0.00486781668694036,0.000245431665326637));
#9378=CARTESIAN_POINT('',(0.005,0.00456439186066706,0.00242440696917958));
#9379=CARTESIAN_POINT('',(0.005,0.00595653458846413,0.000720899227652784));
#9380=CARTESIAN_POINT('',(0.005,0.,0.));
#9381=CARTESIAN_POINT('',(0.005,0.00591835386735469,0.000986451975905453));
#9382=CARTESIAN_POINT('',(0.005,0.00506253629338439,-0.00104026366277788));
#9383=CARTESIAN_POINT('',(0.005,0.004739781998565,0.00113593248306367));
#9384=CARTESIAN_POINT('',(0.005,0.,0.));
#9385=CARTESIAN_POINT('',(0.005,0.00460148981736035,0.0016069123998305));
#9386=CARTESIAN_POINT('',(0.005,0.0036964675448821,0.00361213924144177));
#9387=CARTESIAN_POINT('',(0.005,0.00551215230209143,0.00236984746313938));
#9388=CARTESIAN_POINT('',(0.005,0.,0.));
#9389=CARTESIAN_POINT('',(0.005,0.00540070331371789,0.00261388670703162));
#9390=CARTESIAN_POINT('',(0.005,0.00515054414367435,0.000428155618895864));
#9391=CARTESIAN_POINT('',(0.005,0.00422775836123483,0.00242527013732677));
#9392=CARTESIAN_POINT('',(0.005,0.,0.));
#9393=CARTESIAN_POINT('',(0.005,0.00396237760889146,0.00283821064837611));
#9394=CARTESIAN_POINT('',(0.005,0.00252907741234975,0.00450723747458157));
#9395=CARTESIAN_POINT('',(0.005,0.00462120821823527,0.00382680475118797));
#9396=CARTESIAN_POINT('',(0.005,0.,0.));
#9397=CARTESIAN_POINT('',(0.005,0.004445519896823,0.0040295598825369));
#9398=CARTESIAN_POINT('',(0.005,0.00482128553890928,0.00186188827866618));
#9399=CARTESIAN_POINT('',(0.005,0.00337322688492453,0.00351812682870053));
#9400=CARTESIAN_POINT('',(0.005,0.,0.));
#9401=CARTESIAN_POINT('',(0.005,0.0030022571317172,0.00383957394967895));
#9402=CARTESIAN_POINT('',(0.005,0.00115679646887134,0.00503718613310418));
#9403=CARTESIAN_POINT('',(0.005,0.00335588132792118,0.00497373707717948));
#9404=CARTESIAN_POINT('',(0.005,0.,0.));
#9405=CARTESIAN_POINT('',(0.005,0.00313018689641234,0.00511878208107441));
#9406=CARTESIAN_POINT('',(0.005,0.00410143505307092,0.00314478182317491));
#9407=CARTESIAN_POINT('',(0.005,0.00224541662775037,0.00432596580751884));
#9408=CARTESIAN_POINT('',(0.005,0.,0.));
#9409=CARTESIAN_POINT('',(0.005,0.00179891163684187,0.00452987780440432));
#9410=CARTESIAN_POINT('',(0.005,-0.000309201244781521,0.0051590519284221));
#9411=CARTESIAN_POINT('',(0.005,0.00181868089061367,0.00571772680513127));
#9412=CARTESIAN_POINT('',(0.005,0.,0.));
#9413=CARTESIAN_POINT('',(0.005,0.00156126476959262,0.00579331099797248));
#9414=CARTESIAN_POINT('',(0.005,0.00304931069140623,0.00417290384710765));
#9415=CARTESIAN_POINT('',(0.005,0.00093569606940275,0.00478334076412127));
#9416=CARTESIAN_POINT('',(0.005,0.,0.));
#9417=CARTESIAN_POINT('',(0.005,0.00044982901968905,0.00485319789963748));
#9418=CARTESIAN_POINT('',(0.005,-0.00175014931247279,0.00486296201856248));
#9419=CARTESIAN_POINT('',(0.005,0.000134141743660354,0.00599850031196196));
#9420=CARTESIAN_POINT('',(0.005,0.,0.));
#9421=CARTESIAN_POINT('',(-0.01,0.,0.));
#9422=CARTESIAN_POINT('',(0.0025,-0.000134141743660394,0.00599850031196196));
#9423=CARTESIAN_POINT('',(0.,-0.000134141743660394,0.00599850031196196));
#9424=CARTESIAN_POINT('',(0.0025,0.000134141743660354,0.00599850031196196));
#9425=CARTESIAN_POINT('',(0.,0.000134141743660354,0.00599850031196196));
#9426=CARTESIAN_POINT('',(0.,0.,0.));
#9427=CARTESIAN_POINT('',(-0.01,0.,0.));
#9428=CARTESIAN_POINT('',(0.0025,-0.00156126476959266,0.00579331099797247));
#9429=CARTESIAN_POINT('',(0.,-0.00156126476959266,0.00579331099797247));
#9430=CARTESIAN_POINT('',(0.,0.,0.));
#9431=CARTESIAN_POINT('',(0.,-0.0018186808906137,0.00571772680513126));
#9432=CARTESIAN_POINT('',(0.0025,-0.0018186808906137,0.00571772680513126));
#9433=CARTESIAN_POINT('',(-0.01,0.,0.));
#9434=CARTESIAN_POINT('',(0.0025,0.00156126476959262,0.00579331099797248));
#9435=CARTESIAN_POINT('',(0.,0.00156126476959262,0.00579331099797248));
#9436=CARTESIAN_POINT('',(0.0025,0.00181868089061367,0.00571772680513127));
#9437=CARTESIAN_POINT('',(0.,0.00181868089061367,0.00571772680513127));
#9438=CARTESIAN_POINT('',(0.,0.,0.));
#9439=CARTESIAN_POINT('',(-0.01,0.,0.));
#9440=CARTESIAN_POINT('',(0.0025,0.00313018689641234,0.00511878208107441));
#9441=CARTESIAN_POINT('',(0.,0.00313018689641234,0.00511878208107441));
#9442=CARTESIAN_POINT('',(0.0025,0.00335588132792118,0.00497373707717949));
#9443=CARTESIAN_POINT('',(0.,0.00335588132792118,0.00497373707717949));
#9444=CARTESIAN_POINT('',(0.,0.,0.));
#9445=CARTESIAN_POINT('',(-0.01,0.,0.));
#9446=CARTESIAN_POINT('',(0.0025,0.00540070331371789,0.00261388670703162));
#9447=CARTESIAN_POINT('',(0.,0.00540070331371789,0.00261388670703162));
#9448=CARTESIAN_POINT('',(0.0025,0.00551215230209143,0.00236984746313938));
#9449=CARTESIAN_POINT('',(0.,0.00551215230209143,0.00236984746313938));
#9450=CARTESIAN_POINT('',(0.,0.,0.));
#9451=CARTESIAN_POINT('',(-0.01,0.,0.));
#9452=CARTESIAN_POINT('',(0.0025,0.00462120821823527,0.00382680475118797));
#9453=CARTESIAN_POINT('',(0.,0.00462120821823527,0.00382680475118797));
#9454=CARTESIAN_POINT('',(0.,0.,0.));
#9455=CARTESIAN_POINT('',(0.,0.004445519896823,0.0040295598825369));
#9456=CARTESIAN_POINT('',(0.0025,0.004445519896823,0.0040295598825369));
#9457=CARTESIAN_POINT('',(-0.01,0.,0.));
#9458=CARTESIAN_POINT('',(0.0025,-0.00595653458846414,0.000720899227652746));
#9459=CARTESIAN_POINT('',(0.,-0.00595653458846414,0.000720899227652745));
#9460=CARTESIAN_POINT('',(0.0025,-0.0059183538673547,0.000986451975905412));
#9461=CARTESIAN_POINT('',(0.,-0.0059183538673547,0.000986451975905412));
#9462=CARTESIAN_POINT('',(0.,0.,0.));
#9463=CARTESIAN_POINT('',(-0.01,0.,0.));
#9464=CARTESIAN_POINT('',(0.0025,-0.00595653458846413,-0.000720899227652823));
#9465=CARTESIAN_POINT('',(0.,-0.00595653458846413,-0.000720899227652823));
#9466=CARTESIAN_POINT('',(0.,0.,0.));
#9467=CARTESIAN_POINT('',(0.,-0.00591835386735468,-0.000986451975905493));
#9468=CARTESIAN_POINT('',(0.0025,-0.00591835386735468,-0.000986451975905493));
#9469=CARTESIAN_POINT('',(-0.01,0.,0.));
#9470=CARTESIAN_POINT('',(0.0025,-0.00551215230209144,0.00236984746313935));
#9471=CARTESIAN_POINT('',(0.,-0.00551215230209144,0.00236984746313935));
#9472=CARTESIAN_POINT('',(0.0025,-0.0054007033137179,0.00261388670703158));
#9473=CARTESIAN_POINT('',(0.,-0.0054007033137179,0.00261388670703158));
#9474=CARTESIAN_POINT('',(0.,0.,0.));
#9475=CARTESIAN_POINT('',(-0.01,0.,0.));
#9476=CARTESIAN_POINT('',(0.0025,-0.00462120821823529,0.00382680475118794));
#9477=CARTESIAN_POINT('',(0.,-0.00462120821823529,0.00382680475118794));
#9478=CARTESIAN_POINT('',(0.0025,-0.00444551989682302,0.00402955988253688));
#9479=CARTESIAN_POINT('',(0.,-0.00444551989682302,0.00402955988253688));
#9480=CARTESIAN_POINT('',(0.,0.,0.));
#9481=CARTESIAN_POINT('',(-0.01,0.,0.));
#9482=CARTESIAN_POINT('',(0.0025,-0.00313018689641237,0.00511878208107439));
#9483=CARTESIAN_POINT('',(0.,-0.00313018689641237,0.00511878208107439));
#9484=CARTESIAN_POINT('',(0.,0.,0.));
#9485=CARTESIAN_POINT('',(0.,-0.00335588132792122,0.00497373707717946));
#9486=CARTESIAN_POINT('',(0.0025,-0.00335588132792122,0.00497373707717946));
#9487=CARTESIAN_POINT('',(-0.01,0.,0.));
#9488=CARTESIAN_POINT('',(0.0025,-0.00444551989682297,-0.00402955988253693));
#9489=CARTESIAN_POINT('',(0.,-0.00444551989682297,-0.00402955988253693));
#9490=CARTESIAN_POINT('',(0.0025,-0.00462120821823524,-0.00382680475118801));
#9491=CARTESIAN_POINT('',(0.,-0.00462120821823524,-0.00382680475118801));
#9492=CARTESIAN_POINT('',(0.,0.,0.));
#9493=CARTESIAN_POINT('',(-0.01,0.,0.));
#9494=CARTESIAN_POINT('',(0.0025,-0.00335588132792115,-0.00497373707717951));
#9495=CARTESIAN_POINT('',(0.,-0.00335588132792115,-0.00497373707717951));
#9496=CARTESIAN_POINT('',(0.,0.,0.));
#9497=CARTESIAN_POINT('',(0.,-0.00313018689641231,-0.00511878208107443));
#9498=CARTESIAN_POINT('',(0.0025,-0.00313018689641231,-0.00511878208107443));
#9499=CARTESIAN_POINT('',(-0.01,0.,0.));
#9500=CARTESIAN_POINT('',(0.0025,-0.00181868089061363,-0.00571772680513128));
#9501=CARTESIAN_POINT('',(0.,-0.00181868089061363,-0.00571772680513128));
#9502=CARTESIAN_POINT('',(0.,0.,0.));
#9503=CARTESIAN_POINT('',(0.,-0.00156126476959258,-0.00579331099797249));
#9504=CARTESIAN_POINT('',(0.0025,-0.00156126476959258,-0.00579331099797249));
#9505=CARTESIAN_POINT('',(-0.01,0.,0.));
#9506=CARTESIAN_POINT('',(0.0025,-0.000134141743660315,-0.00599850031196196));
#9507=CARTESIAN_POINT('',(0.,-0.000134141743660315,-0.00599850031196196));
#9508=CARTESIAN_POINT('',(0.,0.,0.));
#9509=CARTESIAN_POINT('',(0.,0.000134141743660435,-0.00599850031196196));
#9510=CARTESIAN_POINT('',(0.0025,0.000134141743660435,-0.00599850031196196));
#9511=CARTESIAN_POINT('',(-0.01,0.,0.));
#9512=CARTESIAN_POINT('',(0.0025,-0.00540070331371787,-0.00261388670703166));
#9513=CARTESIAN_POINT('',(0.,-0.00540070331371787,-0.00261388670703166));
#9514=CARTESIAN_POINT('',(0.0025,-0.00551215230209141,-0.00236984746313942));
#9515=CARTESIAN_POINT('',(0.,-0.00551215230209141,-0.00236984746313941));
#9516=CARTESIAN_POINT('',(0.,0.,0.));
#9517=CARTESIAN_POINT('',(-0.01,0.,0.));
#9518=CARTESIAN_POINT('',(0.0025,0.00335588132792125,-0.00497373707717944));
#9519=CARTESIAN_POINT('',(0.,0.00335588132792125,-0.00497373707717944));
#9520=CARTESIAN_POINT('',(0.0025,0.0031301868964124,-0.00511878208107437));
#9521=CARTESIAN_POINT('',(0.,0.0031301868964124,-0.00511878208107437));
#9522=CARTESIAN_POINT('',(0.,0.,0.));
#9523=CARTESIAN_POINT('',(-0.01,0.,0.));
#9524=CARTESIAN_POINT('',(0.0025,0.00444551989682306,-0.00402955988253685));
#9525=CARTESIAN_POINT('',(0.,0.00444551989682306,-0.00402955988253685));
#9526=CARTESIAN_POINT('',(0.,0.,0.));
#9527=CARTESIAN_POINT('',(0.,0.00462120821823532,-0.00382680475118791));
#9528=CARTESIAN_POINT('',(0.0025,0.00462120821823532,-0.00382680475118791));
#9529=CARTESIAN_POINT('',(-0.01,0.,0.));
#9530=CARTESIAN_POINT('',(0.0025,0.00540070331371792,-0.00261388670703155));
#9531=CARTESIAN_POINT('',(0.,0.00540070331371792,-0.00261388670703155));
#9532=CARTESIAN_POINT('',(0.,0.,0.));
#9533=CARTESIAN_POINT('',(0.,0.00551215230209146,-0.00236984746313931));
#9534=CARTESIAN_POINT('',(0.0025,0.00551215230209146,-0.00236984746313931));
#9535=CARTESIAN_POINT('',(-0.01,0.,0.));
#9536=CARTESIAN_POINT('',(0.0025,0.0059183538673547,-0.000986451975905377));
#9537=CARTESIAN_POINT('',(0.,0.0059183538673547,-0.000986451975905377));
#9538=CARTESIAN_POINT('',(0.,0.,0.));
#9539=CARTESIAN_POINT('',(0.,0.00595653458846413,-0.000720899227652784));
#9540=CARTESIAN_POINT('',(0.0025,0.00595653458846413,-0.000720899227652784));
#9541=CARTESIAN_POINT('',(-0.01,0.,0.));
#9542=CARTESIAN_POINT('',(0.0025,0.00181868089061374,-0.00571772680513125));
#9543=CARTESIAN_POINT('',(0.,0.00181868089061374,-0.00571772680513125));
#9544=CARTESIAN_POINT('',(0.0025,0.00156126476959269,-0.00579331099797246));
#9545=CARTESIAN_POINT('',(0.,0.00156126476959269,-0.00579331099797246));
#9546=CARTESIAN_POINT('',(0.,0.,0.));
#9547=CARTESIAN_POINT('',(0.,0.,0.));
#9548=CARTESIAN_POINT('',(0.,0.00175014931247276,0.00486296201856249));
#9549=CARTESIAN_POINT('',(0.,-0.000449829019689083,0.00485319789963747));
#9550=CARTESIAN_POINT('',(0.,-0.00175014931247279,0.00486296201856248));
#9551=CARTESIAN_POINT('',(0.,0.00044982901968905,0.00485319789963748));
#9552=CARTESIAN_POINT('',(0.,0.,0.));
#9553=CARTESIAN_POINT('',(0.,0.00093569606940275,0.00478334076412127));
#9554=CARTESIAN_POINT('',(0.,0.00304931069140623,0.00417290384710765));
#9555=CARTESIAN_POINT('',(0.,-0.000309201244781521,0.0051590519284221));
#9556=CARTESIAN_POINT('',(0.,0.00179891163684187,0.00452987780440432));
#9557=CARTESIAN_POINT('',(0.,0.,0.));
#9558=CARTESIAN_POINT('',(0.,0.00224541662775037,0.00432596580751884));
#9559=CARTESIAN_POINT('',(0.,0.00410143505307092,0.00314478182317491));
#9560=CARTESIAN_POINT('',(0.,0.00115679646887134,0.00503718613310418));
#9561=CARTESIAN_POINT('',(0.,0.0030022571317172,0.00383957394967895));
#9562=CARTESIAN_POINT('',(0.,0.,0.));
#9563=CARTESIAN_POINT('',(0.,0.00337322688492453,0.00351812682870052));
#9564=CARTESIAN_POINT('',(0.,0.00482128553890928,0.00186188827866618));
#9565=CARTESIAN_POINT('',(0.,0.00252907741234975,0.00450723747458157));
#9566=CARTESIAN_POINT('',(0.,0.00396237760889146,0.00283821064837611));
#9567=CARTESIAN_POINT('',(0.,0.,0.));
#9568=CARTESIAN_POINT('',(0.,0.00422775836123483,0.00242527013732677));
#9569=CARTESIAN_POINT('',(0.,0.00515054414367435,0.000428155618895864));
#9570=CARTESIAN_POINT('',(0.,0.0036964675448821,0.00361213924144177));
#9571=CARTESIAN_POINT('',(0.,0.00460148981736035,0.0016069123998305));
#9572=CARTESIAN_POINT('',(0.,0.,0.));
#9573=CARTESIAN_POINT('',(0.,0.004739781998565,0.00113593248306367));
#9574=CARTESIAN_POINT('',(0.,0.00506253629338439,-0.00104026366277788));
#9575=CARTESIAN_POINT('',(0.,0.00591835386735469,0.000986451975905453));
#9576=CARTESIAN_POINT('',(0.,0.,0.));
#9577=CARTESIAN_POINT('',(0.,0.00595653458846413,0.000720899227652784));
#9578=CARTESIAN_POINT('',(0.,0.00456439186066706,0.00242440696917958));
#9579=CARTESIAN_POINT('',(0.,0.00486781668694036,0.000245431665326637));
#9580=CARTESIAN_POINT('',(0.,0.,0.));
#9581=CARTESIAN_POINT('',(0.,0.00486781668694036,-0.000245431665326637));
#9582=CARTESIAN_POINT('',(0.,0.00456439186066706,-0.00242440696917958));
#9583=CARTESIAN_POINT('',(0.,0.00506253629338438,0.00104026366277795));
#9584=CARTESIAN_POINT('',(0.,0.00473978199856501,-0.00113593248306361));
#9585=CARTESIAN_POINT('',(0.,0.,0.));
#9586=CARTESIAN_POINT('',(0.,0.00460148981736037,-0.00160691239983044));
#9587=CARTESIAN_POINT('',(0.,0.00369646754488215,-0.00361213924144172));
#9588=CARTESIAN_POINT('',(0.,0.00515054414367435,-0.000428155618895793));
#9589=CARTESIAN_POINT('',(0.,0.00422775836123486,-0.00242527013732671));
#9590=CARTESIAN_POINT('',(0.,0.,0.));
#9591=CARTESIAN_POINT('',(0.,0.0039623776088915,-0.00283821064837605));
#9592=CARTESIAN_POINT('',(0.,0.00252907741234981,-0.00450723747458154));
#9593=CARTESIAN_POINT('',(0.,0.0048212855389093,-0.00186188827866611));
#9594=CARTESIAN_POINT('',(0.,0.00337322688492458,-0.00351812682870047));
#9595=CARTESIAN_POINT('',(0.,0.,0.));
#9596=CARTESIAN_POINT('',(0.,0.00300225713171725,-0.00383957394967891));
#9597=CARTESIAN_POINT('',(0.,0.00115679646887141,-0.00503718613310416));
#9598=CARTESIAN_POINT('',(0.,0.00410143505307097,-0.00314478182317485));
#9599=CARTESIAN_POINT('',(0.,0.00224541662775043,-0.00432596580751882));
#9600=CARTESIAN_POINT('',(0.,0.,0.));
#9601=CARTESIAN_POINT('',(0.,0.00179891163684193,-0.0045298778044043));
#9602=CARTESIAN_POINT('',(0.,-0.000309201244781452,-0.0051590519284221));
#9603=CARTESIAN_POINT('',(0.,0.00304931069140629,-0.00417290384710761));
#9604=CARTESIAN_POINT('',(0.,0.000935696069402815,-0.00478334076412126));
#9605=CARTESIAN_POINT('',(0.,0.,0.));
#9606=CARTESIAN_POINT('',(0.,0.000449829019689116,-0.00485319789963747));
#9607=CARTESIAN_POINT('',(0.,-0.00175014931247273,-0.0048629620185625));
#9608=CARTESIAN_POINT('',(0.,0.00175014931247283,-0.00486296201856246));
#9609=CARTESIAN_POINT('',(0.,-0.000449829019689018,-0.00485319789963748));
#9610=CARTESIAN_POINT('',(0.,0.,0.));
#9611=CARTESIAN_POINT('',(0.,-0.000935696069402719,-0.00478334076412128));
#9612=CARTESIAN_POINT('',(0.,-0.0030493106914062,-0.00417290384710767));
#9613=CARTESIAN_POINT('',(0.,0.000309201244781555,-0.0051590519284221));
#9614=CARTESIAN_POINT('',(0.,-0.00179891163684184,-0.00452987780440433));
#9615=CARTESIAN_POINT('',(0.,0.,0.));
#9616=CARTESIAN_POINT('',(0.,-0.00224541662775034,-0.00432596580751886));
#9617=CARTESIAN_POINT('',(0.,-0.0041014350530709,-0.00314478182317494));
#9618=CARTESIAN_POINT('',(0.,-0.00115679646887131,-0.00503718613310418));
#9619=CARTESIAN_POINT('',(0.,-0.00300225713171717,-0.00383957394967897));
#9620=CARTESIAN_POINT('',(0.,0.,0.));
#9621=CARTESIAN_POINT('',(0.,-0.0033732268849245,-0.00351812682870055));
#9622=CARTESIAN_POINT('',(0.,-0.00482128553890927,-0.00186188827866621));
#9623=CARTESIAN_POINT('',(0.,-0.00252907741234972,-0.00450723747458159));
#9624=CARTESIAN_POINT('',(0.,-0.00396237760889144,-0.00283821064837614));
#9625=CARTESIAN_POINT('',(0.,0.,0.));
#9626=CARTESIAN_POINT('',(0.,-0.00422775836123482,-0.0024252701373268));
#9627=CARTESIAN_POINT('',(0.,-0.00515054414367434,-0.0004281556188959));
#9628=CARTESIAN_POINT('',(0.,-0.00369646754488208,-0.00361213924144179));
#9629=CARTESIAN_POINT('',(0.,-0.00460148981736034,-0.00160691239983053));
#9630=CARTESIAN_POINT('',(0.,0.,0.));
#9631=CARTESIAN_POINT('',(0.,-0.00473978199856499,-0.00113593248306371));
#9632=CARTESIAN_POINT('',(0.,-0.0050625362933844,0.00104026366277785));
#9633=CARTESIAN_POINT('',(0.,-0.00456439186066704,-0.00242440696917961));
#9634=CARTESIAN_POINT('',(0.,-0.00486781668694036,-0.000245431665326668));
#9635=CARTESIAN_POINT('',(0.,0.,0.));
#9636=CARTESIAN_POINT('',(0.,-0.00486781668694036,0.000245431665326605));
#9637=CARTESIAN_POINT('',(0.,-0.00456439186066708,0.00242440696917955));
#9638=CARTESIAN_POINT('',(0.,-0.00506253629338438,-0.00104026366277791));
#9639=CARTESIAN_POINT('',(0.,-0.004739781998565,0.00113593248306364));
#9640=CARTESIAN_POINT('',(0.,0.,0.));
#9641=CARTESIAN_POINT('',(0.,-0.00460148981736036,0.00160691239983047));
#9642=CARTESIAN_POINT('',(0.,-0.00369646754488213,0.00361213924144174));
#9643=CARTESIAN_POINT('',(0.,-0.00515054414367435,0.000428155618895829));
#9644=CARTESIAN_POINT('',(0.,-0.00422775836123484,0.00242527013732674));
#9645=CARTESIAN_POINT('',(0.,0.,0.));
#9646=CARTESIAN_POINT('',(0.,-0.00396237760889148,0.00283821064837608));
#9647=CARTESIAN_POINT('',(0.,-0.00252907741234978,0.00450723747458156));
#9648=CARTESIAN_POINT('',(0.,-0.00482128553890929,0.00186188827866615));
#9649=CARTESIAN_POINT('',(0.,-0.00337322688492455,0.0035181268287005));
#9650=CARTESIAN_POINT('',(0.,0.,0.));
#9651=CARTESIAN_POINT('',(0.,-0.00300225713171722,0.00383957394967893));
#9652=CARTESIAN_POINT('',(0.,-0.00115679646887138,0.00503718613310417));
#9653=CARTESIAN_POINT('',(0.,-0.00410143505307095,0.00314478182317488));
#9654=CARTESIAN_POINT('',(0.,-0.0022454166277504,0.00432596580751883));
#9655=CARTESIAN_POINT('',(0.,0.,0.));
#9656=CARTESIAN_POINT('',(0.,-0.0017989116368419,0.00452987780440431));
#9657=CARTESIAN_POINT('',(0.,0.000309201244781488,0.0051590519284221));
#9658=CARTESIAN_POINT('',(0.,-0.00304931069140626,0.00417290384710763));
#9659=CARTESIAN_POINT('',(0.,-0.000935696069402783,0.00478334076412126));
#9660=CARTESIAN_POINT('',(0.,0.,0.));
#9661=CARTESIAN_POINT('',(-0.01,0.,0.));
#9662=CARTESIAN_POINT('',(0.0025,0.00591835386735469,0.000986451975905453));
#9663=CARTESIAN_POINT('',(0.0025,0.00595653458846413,0.000720899227652784));
#9664=CARTESIAN_POINT('',(0.005,0.00456439186066706,-0.00242440696917958));
#9665=CARTESIAN_POINT('',(0.005,0.00486781668694036,-0.000245431665326637));
#9666=CARTESIAN_POINT('',(0.005,0.00456439186066706,0.00242440696917958));
#9667=CARTESIAN_POINT('',(0.005,0.00486781668694036,0.000245431665326637));
#9668=CARTESIAN_POINT('',(0.005,0.,0.));
#9669=CARTESIAN_POINT('',(0.005,0.00506253629338439,-0.00104026366277788));
#9670=CARTESIAN_POINT('',(0.005,0.004739781998565,0.00113593248306367));
#9671=CARTESIAN_POINT('',(0.005,0.0036964675448821,0.00361213924144177));
#9672=CARTESIAN_POINT('',(0.005,0.00460148981736035,0.0016069123998305));
#9673=CARTESIAN_POINT('',(0.005,0.,0.));
#9674=CARTESIAN_POINT('',(0.005,-0.00175014931247273,-0.0048629620185625));
#9675=CARTESIAN_POINT('',(0.005,0.000449829019689116,-0.00485319789963747));
#9676=CARTESIAN_POINT('',(0.005,0.00304931069140629,-0.00417290384710761));
#9677=CARTESIAN_POINT('',(0.005,0.000935696069402815,-0.00478334076412126));
#9678=CARTESIAN_POINT('',(0.005,0.,0.));
#9679=CARTESIAN_POINT('',(0.005,-0.000309201244781452,-0.0051590519284221));
#9680=CARTESIAN_POINT('',(0.005,0.00179891163684193,-0.0045298778044043));
#9681=CARTESIAN_POINT('',(0.005,0.00410143505307097,-0.00314478182317485));
#9682=CARTESIAN_POINT('',(0.005,0.00224541662775043,-0.00432596580751882));
#9683=CARTESIAN_POINT('',(0.005,0.,0.));
#9684=CARTESIAN_POINT('',(0.005,0.00369646754488215,-0.00361213924144172));
#9685=CARTESIAN_POINT('',(0.005,0.00460148981736037,-0.00160691239983044));
#9686=CARTESIAN_POINT('',(0.005,0.00506253629338438,0.00104026366277795));
#9687=CARTESIAN_POINT('',(0.005,0.00473978199856501,-0.00113593248306361));
#9688=CARTESIAN_POINT('',(0.005,0.,0.));
#9689=CARTESIAN_POINT('',(0.005,0.00252907741234981,-0.00450723747458154));
#9690=CARTESIAN_POINT('',(0.005,0.0039623776088915,-0.00283821064837605));
#9691=CARTESIAN_POINT('',(0.005,0.00515054414367435,-0.000428155618895793));
#9692=CARTESIAN_POINT('',(0.005,0.00422775836123486,-0.00242527013732671));
#9693=CARTESIAN_POINT('',(0.005,0.,0.));
#9694=CARTESIAN_POINT('',(0.005,0.00115679646887141,-0.00503718613310416));
#9695=CARTESIAN_POINT('',(0.005,0.00300225713171725,-0.00383957394967891));
#9696=CARTESIAN_POINT('',(0.005,0.0048212855389093,-0.00186188827866611));
#9697=CARTESIAN_POINT('',(0.005,0.00337322688492458,-0.00351812682870047));
#9698=CARTESIAN_POINT('',(0.005,0.,0.));
#9699=CARTESIAN_POINT('',(0.005,-0.0050625362933844,0.00104026366277785));
#9700=CARTESIAN_POINT('',(0.005,-0.00473978199856499,-0.00113593248306371));
#9701=CARTESIAN_POINT('',(0.005,-0.00369646754488208,-0.00361213924144179));
#9702=CARTESIAN_POINT('',(0.005,-0.00460148981736034,-0.00160691239983053));
#9703=CARTESIAN_POINT('',(0.005,0.,0.));
#9704=CARTESIAN_POINT('',(0.005,-0.00515054414367434,-0.0004281556188959));
#9705=CARTESIAN_POINT('',(0.005,-0.00422775836123482,-0.0024252701373268));
#9706=CARTESIAN_POINT('',(0.005,-0.00252907741234972,-0.00450723747458159));
#9707=CARTESIAN_POINT('',(0.005,-0.00396237760889144,-0.00283821064837614));
#9708=CARTESIAN_POINT('',(0.005,0.,0.));
#9709=CARTESIAN_POINT('',(0.005,-0.0030493106914062,-0.00417290384710767));
#9710=CARTESIAN_POINT('',(0.005,-0.000935696069402719,-0.00478334076412128));
#9711=CARTESIAN_POINT('',(0.005,0.00175014931247283,-0.00486296201856246));
#9712=CARTESIAN_POINT('',(0.005,-0.000449829019689018,-0.00485319789963748));
#9713=CARTESIAN_POINT('',(0.005,0.,0.));
#9714=CARTESIAN_POINT('',(0.005,-0.0041014350530709,-0.00314478182317494));
#9715=CARTESIAN_POINT('',(0.005,-0.00224541662775034,-0.00432596580751886));
#9716=CARTESIAN_POINT('',(0.005,0.000309201244781555,-0.0051590519284221));
#9717=CARTESIAN_POINT('',(0.005,-0.00179891163684184,-0.00452987780440433));
#9718=CARTESIAN_POINT('',(0.005,0.,0.));
#9719=CARTESIAN_POINT('',(0.005,-0.00482128553890927,-0.00186188827866621));
#9720=CARTESIAN_POINT('',(0.005,-0.0033732268849245,-0.00351812682870055));
#9721=CARTESIAN_POINT('',(0.005,-0.00115679646887131,-0.00503718613310418));
#9722=CARTESIAN_POINT('',(0.005,-0.00300225713171717,-0.00383957394967897));
#9723=CARTESIAN_POINT('',(0.005,0.,0.));
#9724=CARTESIAN_POINT('',(0.005,-0.00115679646887138,0.00503718613310417));
#9725=CARTESIAN_POINT('',(0.005,-0.00300225713171722,0.00383957394967893));
#9726=CARTESIAN_POINT('',(0.005,-0.00482128553890929,0.00186188827866615));
#9727=CARTESIAN_POINT('',(0.005,-0.00337322688492455,0.0035181268287005));
#9728=CARTESIAN_POINT('',(0.005,0.,0.));
#9729=CARTESIAN_POINT('',(0.005,0.000309201244781488,0.0051590519284221));
#9730=CARTESIAN_POINT('',(0.005,-0.0017989116368419,0.00452987780440431));
#9731=CARTESIAN_POINT('',(0.005,-0.00410143505307095,0.00314478182317488));
#9732=CARTESIAN_POINT('',(0.005,-0.0022454166277504,0.00432596580751883));
#9733=CARTESIAN_POINT('',(0.005,0.,0.));
#9734=CARTESIAN_POINT('',(0.005,-0.00252907741234978,0.00450723747458156));
#9735=CARTESIAN_POINT('',(0.005,-0.00396237760889148,0.00283821064837608));
#9736=CARTESIAN_POINT('',(0.005,-0.00515054414367435,0.000428155618895829));
#9737=CARTESIAN_POINT('',(0.005,-0.00422775836123484,0.00242527013732674));
#9738=CARTESIAN_POINT('',(0.005,0.,0.));
#9739=CARTESIAN_POINT('',(0.005,-0.00369646754488213,0.00361213924144174));
#9740=CARTESIAN_POINT('',(0.005,-0.00460148981736036,0.00160691239983047));
#9741=CARTESIAN_POINT('',(0.005,-0.00506253629338438,-0.00104026366277791));
#9742=CARTESIAN_POINT('',(0.005,-0.004739781998565,0.00113593248306364));
#9743=CARTESIAN_POINT('',(0.005,0.,0.));
#9744=CARTESIAN_POINT('',(0.005,-0.00456439186066708,0.00242440696917955));
#9745=CARTESIAN_POINT('',(0.005,-0.00486781668694036,0.000245431665326605));
#9746=CARTESIAN_POINT('',(0.005,-0.00456439186066704,-0.00242440696917961));
#9747=CARTESIAN_POINT('',(0.005,-0.00486781668694036,-0.000245431665326668));
#9748=CARTESIAN_POINT('',(0.005,0.,0.));
#9749=CARTESIAN_POINT('',(0.005,0.00482128553890928,0.00186188827866618));
#9750=CARTESIAN_POINT('',(0.005,0.00337322688492453,0.00351812682870053));
#9751=CARTESIAN_POINT('',(0.005,0.00115679646887134,0.00503718613310418));
#9752=CARTESIAN_POINT('',(0.005,0.0030022571317172,0.00383957394967895));
#9753=CARTESIAN_POINT('',(0.005,0.,0.));
#9754=CARTESIAN_POINT('',(0.005,0.00515054414367435,0.000428155618895864));
#9755=CARTESIAN_POINT('',(0.005,0.00422775836123483,0.00242527013732677));
#9756=CARTESIAN_POINT('',(0.005,0.00252907741234975,0.00450723747458157));
#9757=CARTESIAN_POINT('',(0.005,0.00396237760889146,0.00283821064837611));
#9758=CARTESIAN_POINT('',(0.005,0.,0.));
#9759=CARTESIAN_POINT('',(0.005,0.00410143505307092,0.00314478182317491));
#9760=CARTESIAN_POINT('',(0.005,0.00224541662775037,0.00432596580751884));
#9761=CARTESIAN_POINT('',(0.005,-0.000309201244781521,0.0051590519284221));
#9762=CARTESIAN_POINT('',(0.005,0.00179891163684187,0.00452987780440432));
#9763=CARTESIAN_POINT('',(0.005,0.,0.));
#9764=CARTESIAN_POINT('',(0.005,0.00304931069140623,0.00417290384710765));
#9765=CARTESIAN_POINT('',(0.005,0.00093569606940275,0.00478334076412127));
#9766=CARTESIAN_POINT('',(0.005,-0.00175014931247279,0.00486296201856248));
#9767=CARTESIAN_POINT('',(0.005,0.00044982901968905,0.00485319789963748));
#9768=CARTESIAN_POINT('',(0.005,0.,0.));
#9769=CARTESIAN_POINT('',(0.005,0.00175014931247276,0.00486296201856249));
#9770=CARTESIAN_POINT('',(0.005,-0.000449829019689083,0.00485319789963747));
#9771=CARTESIAN_POINT('',(0.005,-0.00304931069140626,0.00417290384710763));
#9772=CARTESIAN_POINT('',(0.005,-0.000935696069402783,0.00478334076412126));
#9773=CARTESIAN_POINT('',(0.005,0.,0.));
#9774=CARTESIAN_POINT('',(0.013,0.,0.));
#9775=CARTESIAN_POINT('',(0.013,0.,0.));
#9776=CARTESIAN_POINT('',(0.013,0.,-0.0025));
#9777=CARTESIAN_POINT('',(0.013,0.,0.));
#9778=CARTESIAN_POINT('',(0.013,0.,-0.00375738138352587));
#9779=CARTESIAN_POINT('',(0.01,0.,0.));
#9780=CARTESIAN_POINT('',(0.01,0.,0.));
#9781=CARTESIAN_POINT('',(0.01,0.,-0.00375738138352587));
#9782=CARTESIAN_POINT('',(0.01,0.,0.));
#9783=CARTESIAN_POINT('',(0.01,0.,0.));
#9784=CARTESIAN_POINT('',(0.0500000508,0.,0.));
#9785=CARTESIAN_POINT('',(0.013,0.,0.));
#9786=CARTESIAN_POINT('',(0.013,0.,-0.0015));
#9787=CARTESIAN_POINT('',(0.015,0.,0.));
#9788=CARTESIAN_POINT('',(0.015,0.,-0.0015));
#9789=CARTESIAN_POINT('',(0.015,0.,0.));
#9790=CARTESIAN_POINT('',(0.015,0.,0.));
#9791=CARTESIAN_POINT('',(0.015,0.,-0.0025));
#9792=CARTESIAN_POINT('',(0.015,0.,0.));
#9793=CARTESIAN_POINT('',(0.013,0.,0.));
#10141=MECHANICAL_DESIGN_GEOMETRIC_PRESENTATION_REPRESENTATION('',(#5560),#10142);
#10142=(
GEOMETRIC_REPRESENTATION_CONTEXT(3)
GLOBAL_UNCERTAINTY_ASSIGNED_CONTEXT((#10158))
GLOBAL_UNIT_ASSIGNED_CONTEXT((#10176,#10175,#10174))
REPRESENTATION_CONTEXT('MAS-674','TOP_LEVEL_ASSEMBLY_PART')
);
#10150=(
GEOMETRIC_REPRESENTATION_CONTEXT(3)
GLOBAL_UNCERTAINTY_ASSIGNED_CONTEXT((#10166))
GLOBAL_UNIT_ASSIGNED_CONTEXT((#10176,#10175,#10174))
REPRESENTATION_CONTEXT('Part 1','COMPONENT_PART')
);
#10158=UNCERTAINTY_MEASURE_WITH_UNIT(LENGTH_MEASURE(1.E-8),#10176,
'DISTANCE_ACCURACY_VALUE','Maximum Tolerance applied to model');
#10166=UNCERTAINTY_MEASURE_WITH_UNIT(LENGTH_MEASURE(1.E-8),#10176,
'DISTANCE_ACCURACY_VALUE','Maximum Tolerance applied to model');
#10174=(
NAMED_UNIT(*)
SI_UNIT($,.STERADIAN.)
SOLID_ANGLE_UNIT()
);
#10175=(
NAMED_UNIT(*)
PLANE_ANGLE_UNIT()
SI_UNIT($,.RADIAN.)
);
#10176=(
LENGTH_UNIT()
NAMED_UNIT(*)
SI_UNIT($,.METRE.)
);
#10194=PRODUCT_DEFINITION_SHAPE('','',#10218);
#10218=PRODUCT_DEFINITION('','',#10250,#10234);
#10234=PRODUCT_DEFINITION_CONTEXT('',#10323,'design');
#10250=PRODUCT_DEFINITION_FORMATION_WITH_SPECIFIED_SOURCE('','',#10282,
 .NOT_KNOWN.);
#10282=PRODUCT('Part 1','Part 1','Part 1',(#10314));
#10314=PRODUCT_CONTEXT('',#10323,'mechanical');
#10323=APPLICATION_CONTEXT('managed model based 3d engineering');
ENDSEC;
END-ISO-10303-21;
